ISO-10303-21;
HEADER;
/* Generated by software containing ST-Developer
 * from STEP Tools, Inc. (www.steptools.com) 
 */

FILE_DESCRIPTION(
/* description */ (''),
/* implementation_level */ '2;1');

FILE_NAME(
/* name */ '19_Window_Screw_ISO_7380_M5x10.step',
/* time_stamp */ '2026-10-26T04:15:57-07:00',
/* author */ (''),
/* organization */ (''),
/* preprocessor_version */ 'ST-DEVELOPER v20.2',
/* originating_system */ 'Autodesk Translation Framework v15.15.0.0',
/* authorisation */ '');

FILE_SCHEMA (('AUTOMOTIVE_DESIGN { 1 0 10303 214 3 1 1 }'));
ENDSEC;

DATA;
#10=MECHANICAL_DESIGN_GEOMETRIC_PRESENTATION_REPRESENTATION('',(#471),#55737);
#196=(
BOUNDED_CURVE()
B_SPLINE_CURVE(2,(#55655,#55656,#55657),.UNSPECIFIED.,.F.,.F.)
B_SPLINE_CURVE_WITH_KNOTS((3,3),(-1.3174441897901,-0.379169323323544),
 .UNSPECIFIED.)
CURVE()
GEOMETRIC_REPRESENTATION_ITEM()
RATIONAL_B_SPLINE_CURVE((0.987233104755384,0.885817457260044,1.))
REPRESENTATION_ITEM('')
);
#411=CONICAL_SURFACE('',#29935,2.35,0.785398163397447);
#431=SHAPE_REPRESENTATION_RELATIONSHIP('SRR','None',#55840,#451);
#451=ADVANCED_BREP_SHAPE_REPRESENTATION('',(#491),#55736);
#471=STYLED_ITEM('',(#55998),#491);
#491=MANIFOLD_SOLID_BREP('Body1',#27240);
#582=B_SPLINE_SURFACE_WITH_KNOTS('',3,3,((#54525,#54526,#54527,#54528,#54529,
#54530,#54531,#54532,#54533,#54534,#54535,#54536,#54537,#54538,#54539,#54540,
#54541,#54542,#54543,#54544,#54545,#54546,#54547,#54548,#54549,#54550,#54551,
#54552,#54553,#54554,#54555,#54556,#54557,#54558,#54559,#54560,#54561,#54562,
#54563,#54564,#54565,#54566,#54567,#54568,#54569,#54570,#54571,#54572,#54573,
#54574,#54575,#54576,#54577,#54578,#54579,#54580,#54581,#54582,#54583,#54584,
#54585,#54586,#54587,#54588,#54589,#54590,#54591,#54592,#54593,#54594,#54595,
#54596,#54597,#54598,#54599,#54600,#54601,#54602,#54603,#54604,#54605,#54606),
(#54607,#54608,#54609,#54610,#54611,#54612,#54613,#54614,#54615,#54616,
#54617,#54618,#54619,#54620,#54621,#54622,#54623,#54624,#54625,#54626,#54627,
#54628,#54629,#54630,#54631,#54632,#54633,#54634,#54635,#54636,#54637,#54638,
#54639,#54640,#54641,#54642,#54643,#54644,#54645,#54646,#54647,#54648,#54649,
#54650,#54651,#54652,#54653,#54654,#54655,#54656,#54657,#54658,#54659,#54660,
#54661,#54662,#54663,#54664,#54665,#54666,#54667,#54668,#54669,#54670,#54671,
#54672,#54673,#54674,#54675,#54676,#54677,#54678,#54679,#54680,#54681,#54682,
#54683,#54684,#54685,#54686,#54687,#54688),(#54689,#54690,#54691,#54692,
#54693,#54694,#54695,#54696,#54697,#54698,#54699,#54700,#54701,#54702,#54703,
#54704,#54705,#54706,#54707,#54708,#54709,#54710,#54711,#54712,#54713,#54714,
#54715,#54716,#54717,#54718,#54719,#54720,#54721,#54722,#54723,#54724,#54725,
#54726,#54727,#54728,#54729,#54730,#54731,#54732,#54733,#54734,#54735,#54736,
#54737,#54738,#54739,#54740,#54741,#54742,#54743,#54744,#54745,#54746,#54747,
#54748,#54749,#54750,#54751,#54752,#54753,#54754,#54755,#54756,#54757,#54758,
#54759,#54760,#54761,#54762,#54763,#54764,#54765,#54766,#54767,#54768,#54769,
#54770),(#54771,#54772,#54773,#54774,#54775,#54776,#54777,#54778,#54779,
#54780,#54781,#54782,#54783,#54784,#54785,#54786,#54787,#54788,#54789,#54790,
#54791,#54792,#54793,#54794,#54795,#54796,#54797,#54798,#54799,#54800,#54801,
#54802,#54803,#54804,#54805,#54806,#54807,#54808,#54809,#54810,#54811,#54812,
#54813,#54814,#54815,#54816,#54817,#54818,#54819,#54820,#54821,#54822,#54823,
#54824,#54825,#54826,#54827,#54828,#54829,#54830,#54831,#54832,#54833,#54834,
#54835,#54836,#54837,#54838,#54839,#54840,#54841,#54842,#54843,#54844,#54845,
#54846,#54847,#54848,#54849,#54850,#54851,#54852)),.UNSPECIFIED.,.F.,.F.,
 .F.,(4,4),(4,1,1,1,1,1,1,1,1,1,1,1,1,1,1,1,1,1,1,1,1,1,1,1,1,1,1,1,1,1,
1,1,1,1,1,1,1,1,1,1,1,1,1,1,1,1,1,1,1,1,1,1,1,1,1,1,1,1,1,1,1,1,1,1,1,1,
1,1,1,1,1,1,1,1,1,1,1,1,1,4),(0.,0.0526254770366343),(8.30815772716264,
9.30358800046718,10.2990182737717,11.2944485470763,12.2898788203808,13.2853090936853,
14.2807393669899,15.2761696402944,16.271599913599,17.2670301869035,18.262460460208,
19.2578907335126,20.2533210068171,21.2487512801216,22.2441815534262,23.2396118267307,
24.2350421000353,25.2304723733398,26.2259026466443,27.2213329199489,28.2167631932534,
29.212193466558,30.2076237398625,31.203054013167,32.1984842864716,33.1939145597761,
34.1893448330807,35.1847751063852,36.1802053796897,37.1756356529943,38.1710659262988,
39.1664961996033,40.1619264729079,41.1573567462124,42.152787019517,43.1482172928215,
44.143647566126,45.1390778394306,46.1345081127351,47.1299383860397,48.1253686593442,
49.1207989326487,50.1162292059533,51.1116594792578,52.1070897525623,53.1025200258669,
54.0979502991714,55.093380572476,56.0888108457805,57.084241119085,58.0796713923896,
59.0751016656941,60.0705319389987,61.0659622123032,62.0613924856077,63.0568227589123,
64.0522530322168,65.0476833055214,66.0431135788259,67.0385438521304,68.033974125435,
69.0294043987395,70.0248346720441,71.0202649453486,72.0156952186531,73.0111254919577,
74.0065557652622,75.0019860385667,75.9974163118713,76.9928465851758,77.9882768584804,
78.9837071317849,79.9791374050894,80.974567678394,81.9699979516985,82.9654282250031,
83.9608584983076,84.9562887716121,85.9517190449167,86.9471493182212),
 .UNSPECIFIED.);
#583=B_SPLINE_SURFACE_WITH_KNOTS('',3,3,((#55138,#55139,#55140,#55141,#55142,
#55143,#55144,#55145,#55146,#55147,#55148,#55149,#55150,#55151,#55152,#55153,
#55154,#55155,#55156,#55157,#55158,#55159,#55160,#55161,#55162,#55163,#55164,
#55165,#55166,#55167,#55168,#55169,#55170,#55171,#55172,#55173,#55174,#55175,
#55176,#55177,#55178,#55179,#55180,#55181,#55182,#55183,#55184,#55185,#55186,
#55187,#55188,#55189,#55190,#55191,#55192,#55193,#55194,#55195,#55196,#55197,
#55198,#55199,#55200,#55201,#55202,#55203,#55204,#55205,#55206,#55207,#55208,
#55209,#55210,#55211,#55212,#55213,#55214,#55215,#55216,#55217,#55218,#55219),
(#55220,#55221,#55222,#55223,#55224,#55225,#55226,#55227,#55228,#55229,
#55230,#55231,#55232,#55233,#55234,#55235,#55236,#55237,#55238,#55239,#55240,
#55241,#55242,#55243,#55244,#55245,#55246,#55247,#55248,#55249,#55250,#55251,
#55252,#55253,#55254,#55255,#55256,#55257,#55258,#55259,#55260,#55261,#55262,
#55263,#55264,#55265,#55266,#55267,#55268,#55269,#55270,#55271,#55272,#55273,
#55274,#55275,#55276,#55277,#55278,#55279,#55280,#55281,#55282,#55283,#55284,
#55285,#55286,#55287,#55288,#55289,#55290,#55291,#55292,#55293,#55294,#55295,
#55296,#55297,#55298,#55299,#55300,#55301),(#55302,#55303,#55304,#55305,
#55306,#55307,#55308,#55309,#55310,#55311,#55312,#55313,#55314,#55315,#55316,
#55317,#55318,#55319,#55320,#55321,#55322,#55323,#55324,#55325,#55326,#55327,
#55328,#55329,#55330,#55331,#55332,#55333,#55334,#55335,#55336,#55337,#55338,
#55339,#55340,#55341,#55342,#55343,#55344,#55345,#55346,#55347,#55348,#55349,
#55350,#55351,#55352,#55353,#55354,#55355,#55356,#55357,#55358,#55359,#55360,
#55361,#55362,#55363,#55364,#55365,#55366,#55367,#55368,#55369,#55370,#55371,
#55372,#55373,#55374,#55375,#55376,#55377,#55378,#55379,#55380,#55381,#55382,
#55383),(#55384,#55385,#55386,#55387,#55388,#55389,#55390,#55391,#55392,
#55393,#55394,#55395,#55396,#55397,#55398,#55399,#55400,#55401,#55402,#55403,
#55404,#55405,#55406,#55407,#55408,#55409,#55410,#55411,#55412,#55413,#55414,
#55415,#55416,#55417,#55418,#55419,#55420,#55421,#55422,#55423,#55424,#55425,
#55426,#55427,#55428,#55429,#55430,#55431,#55432,#55433,#55434,#55435,#55436,
#55437,#55438,#55439,#55440,#55441,#55442,#55443,#55444,#55445,#55446,#55447,
#55448,#55449,#55450,#55451,#55452,#55453,#55454,#55455,#55456,#55457,#55458,
#55459,#55460,#55461,#55462,#55463,#55464,#55465)),.UNSPECIFIED.,.F.,.F.,
 .F.,(4,4),(4,1,1,1,1,1,1,1,1,1,1,1,1,1,1,1,1,1,1,1,1,1,1,1,1,1,1,1,1,1,
1,1,1,1,1,1,1,1,1,1,1,1,1,1,1,1,1,1,1,1,1,1,1,1,1,1,1,1,1,1,1,1,1,1,1,1,
1,1,1,1,1,1,1,1,1,1,1,1,1,4),(0.,0.0526254770366344),(11.6163931973414,
12.611823470646,13.6072537439505,14.6026840172551,15.5981142905596,16.5935445638641,
17.5889748371687,18.5844051104732,19.5798353837777,20.5752656570823,21.5706959303868,
22.5661262036914,23.5615564769959,24.5569867503004,25.552417023605,26.5478472969095,
27.5432775702141,28.5387078435186,29.5341381168231,30.5295683901277,31.5249986634322,
32.5204289367368,33.5158592100413,34.5112894833458,35.5067197566504,36.5021500299549,
37.4975803032595,38.493010576564,39.4884408498685,40.4838711231731,41.4793013964776,
42.4747316697821,43.4701619430867,44.4655922163912,45.4610224896958,46.4564527630003,
47.4518830363048,48.4473133096094,49.4427435829139,50.4381738562185,51.433604129523,
52.4290344028275,53.4244646761321,54.4198949494366,55.4153252227412,56.4107554960457,
57.4061857693502,58.4016160426548,59.3970463159593,60.3924765892639,61.3879068625684,
62.3833371358729,63.3787674091775,64.374197682482,65.3696279557865,66.3650582290911,
67.3604885023956,68.3559187757002,69.3513490490047,70.3467793223092,71.3422095956138,
72.3376398689183,73.3330701422229,74.3285004155274,75.3239306888319,76.3193609621365,
77.314791235441,78.3102215087456,79.3056517820501,80.3010820553546,81.2965123286592,
82.2919426019637,83.2873728752682,84.2828031485728,85.2782334218773,86.2736636951819,
87.2690939684864,88.2645242417909,89.2599545150955,90.2553847884),
 .UNSPECIFIED.);
#604=(
BOUNDED_SURFACE()
B_SPLINE_SURFACE(2,2,((#55628,#55629,#55630,#55631,#55632,#55633,#55634,
#55635,#55636),(#55637,#55638,#55639,#55640,#55641,#55642,#55643,#55644,
#55645),(#55646,#55647,#55648,#55649,#55650,#55651,#55652,#55653,#55654)),
 .UNSPECIFIED.,.F.,.T.,.F.)
B_SPLINE_SURFACE_WITH_KNOTS((3,3),(3,2,2,2,3),(0.379169323323544,1.37300521707777),
(-3.14159265358979,-1.5707963267949,0.,1.5707963267949,3.14159265358979),
 .UNSPECIFIED.)
GEOMETRIC_REPRESENTATION_ITEM()
RATIONAL_B_SPLINE_SURFACE(((1.,0.707106781186548,1.,0.707106781186548,1.,
0.707106781186548,1.,0.707106781186548,1.),(0.879056006431844,0.621586463190722,
0.879056006431844,0.621586463190722,0.879056006431844,0.621586463190722,
0.879056006431844,0.621586463190722,0.879056006431844),(1.,0.707106781186548,
1.,0.707106781186548,1.,0.707106781186548,1.,0.707106781186548,1.)))
REPRESENTATION_ITEM('')
SURFACE()
);
#756=FACE_BOUND('',#10117,.T.);
#1748=PLANE('',#29921);
#1749=PLANE('',#29926);
#1750=PLANE('',#29927);
#1751=PLANE('',#29928);
#1752=PLANE('',#29929);
#1753=PLANE('',#29930);
#1754=PLANE('',#29931);
#1755=PLANE('',#29932);
#1756=PLANE('',#29933);
#1757=PLANE('',#29938);
#4091=LINE('',#53621,#6462);
#4092=LINE('',#53645,#6463);
#4093=LINE('',#53693,#6464);
#4094=LINE('',#53741,#6465);
#4095=LINE('',#53795,#6466);
#4096=LINE('',#53843,#6467);
#4097=LINE('',#53891,#6468);
#4098=LINE('',#53939,#6469);
#4099=LINE('',#53993,#6470);
#4100=LINE('',#54041,#6471);
#4101=LINE('',#54089,#6472);
#4102=LINE('',#54143,#6473);
#4103=LINE('',#54191,#6474);
#4104=LINE('',#54238,#6475);
#4105=LINE('',#54258,#6476);
#4106=LINE('',#54282,#6477);
#4107=LINE('',#54307,#6478);
#4108=LINE('',#54332,#6479);
#4109=LINE('',#54356,#6480);
#4110=LINE('',#54381,#6481);
#4111=LINE('',#54406,#6482);
#4112=LINE('',#54430,#6483);
#4113=LINE('',#54454,#6484);
#4114=LINE('',#54479,#6485);
#4115=LINE('',#54504,#6486);
#4116=LINE('',#55561,#6487);
#4117=LINE('',#55563,#6488);
#4118=LINE('',#55564,#6489);
#4119=LINE('',#55574,#6490);
#4120=LINE('',#55575,#6491);
#4121=LINE('',#55585,#6492);
#4122=LINE('',#55586,#6493);
#4123=LINE('',#55596,#6494);
#4124=LINE('',#55597,#6495);
#4125=LINE('',#55607,#6496);
#4126=LINE('',#55608,#6497);
#4127=LINE('',#55616,#6498);
#4128=LINE('',#55622,#6499);
#6462=VECTOR('',#37173,2.5);
#6463=VECTOR('',#37178,2.5);
#6464=VECTOR('',#37181,2.5);
#6465=VECTOR('',#37184,2.5);
#6466=VECTOR('',#37187,2.5);
#6467=VECTOR('',#37190,2.5);
#6468=VECTOR('',#37193,2.5);
#6469=VECTOR('',#37196,2.5);
#6470=VECTOR('',#37199,2.5);
#6471=VECTOR('',#37202,2.5);
#6472=VECTOR('',#37205,2.5);
#6473=VECTOR('',#37208,2.5);
#6474=VECTOR('',#37211,2.5);
#6475=VECTOR('',#37216,1.99475);
#6476=VECTOR('',#37221,1.99475);
#6477=VECTOR('',#37224,1.99475);
#6478=VECTOR('',#37227,1.99475);
#6479=VECTOR('',#37230,1.99475);
#6480=VECTOR('',#37233,1.99475);
#6481=VECTOR('',#37236,1.99475);
#6482=VECTOR('',#37239,1.99475);
#6483=VECTOR('',#37242,1.99475);
#6484=VECTOR('',#37245,1.99475);
#6485=VECTOR('',#37248,1.99475);
#6486=VECTOR('',#37251,1.99475);
#6487=VECTOR('',#37264,10.);
#6488=VECTOR('',#37265,10.);
#6489=VECTOR('',#37266,10.);
#6490=VECTOR('',#37269,10.);
#6491=VECTOR('',#37270,10.);
#6492=VECTOR('',#37273,10.);
#6493=VECTOR('',#37274,10.);
#6494=VECTOR('',#37277,10.);
#6495=VECTOR('',#37278,10.);
#6496=VECTOR('',#37281,10.);
#6497=VECTOR('',#37282,10.);
#6498=VECTOR('',#37285,10.);
#6499=VECTOR('',#37294,2.35);
#6800=CYLINDRICAL_SURFACE('',#29893,2.4505);
#6801=CYLINDRICAL_SURFACE('',#29895,2.4505);
#6802=CYLINDRICAL_SURFACE('',#29896,2.4505);
#6803=CYLINDRICAL_SURFACE('',#29897,2.4505);
#6804=CYLINDRICAL_SURFACE('',#29898,2.4505);
#6805=CYLINDRICAL_SURFACE('',#29899,2.4505);
#6806=CYLINDRICAL_SURFACE('',#29900,2.4505);
#6807=CYLINDRICAL_SURFACE('',#29901,2.4505);
#6808=CYLINDRICAL_SURFACE('',#29902,2.4505);
#6809=CYLINDRICAL_SURFACE('',#29903,2.4505);
#6810=CYLINDRICAL_SURFACE('',#29904,2.4505);
#6811=CYLINDRICAL_SURFACE('',#29905,2.4505);
#6812=CYLINDRICAL_SURFACE('',#29906,2.4505);
#6813=CYLINDRICAL_SURFACE('',#29908,1.99475);
#6814=CYLINDRICAL_SURFACE('',#29910,1.99475);
#6815=CYLINDRICAL_SURFACE('',#29911,1.99475);
#6816=CYLINDRICAL_SURFACE('',#29912,1.99475);
#6817=CYLINDRICAL_SURFACE('',#29913,1.99475);
#6818=CYLINDRICAL_SURFACE('',#29914,1.99475);
#6819=CYLINDRICAL_SURFACE('',#29915,1.99475);
#6820=CYLINDRICAL_SURFACE('',#29916,1.99475);
#6821=CYLINDRICAL_SURFACE('',#29917,1.99475);
#6822=CYLINDRICAL_SURFACE('',#29918,1.99475);
#6823=CYLINDRICAL_SURFACE('',#29919,1.99475);
#6824=CYLINDRICAL_SURFACE('',#29920,1.99475);
#6825=CYLINDRICAL_SURFACE('',#29925,1.99475);
#6826=CYLINDRICAL_SURFACE('',#29936,2.4505);
#8356=FACE_OUTER_BOUND('',#10077,.T.);
#8357=FACE_OUTER_BOUND('',#10078,.T.);
#8358=FACE_OUTER_BOUND('',#10079,.T.);
#8359=FACE_OUTER_BOUND('',#10080,.T.);
#8360=FACE_OUTER_BOUND('',#10081,.T.);
#8361=FACE_OUTER_BOUND('',#10082,.T.);
#8362=FACE_OUTER_BOUND('',#10083,.T.);
#8363=FACE_OUTER_BOUND('',#10084,.T.);
#8364=FACE_OUTER_BOUND('',#10085,.T.);
#8365=FACE_OUTER_BOUND('',#10086,.T.);
#8366=FACE_OUTER_BOUND('',#10087,.T.);
#8367=FACE_OUTER_BOUND('',#10088,.T.);
#8368=FACE_OUTER_BOUND('',#10089,.T.);
#8369=FACE_OUTER_BOUND('',#10090,.T.);
#8370=FACE_OUTER_BOUND('',#10091,.T.);
#8371=FACE_OUTER_BOUND('',#10092,.T.);
#8372=FACE_OUTER_BOUND('',#10093,.T.);
#8373=FACE_OUTER_BOUND('',#10094,.T.);
#8374=FACE_OUTER_BOUND('',#10095,.T.);
#8375=FACE_OUTER_BOUND('',#10096,.T.);
#8376=FACE_OUTER_BOUND('',#10097,.T.);
#8377=FACE_OUTER_BOUND('',#10098,.T.);
#8378=FACE_OUTER_BOUND('',#10099,.T.);
#8379=FACE_OUTER_BOUND('',#10100,.T.);
#8380=FACE_OUTER_BOUND('',#10101,.T.);
#8381=FACE_OUTER_BOUND('',#10102,.T.);
#8382=FACE_OUTER_BOUND('',#10103,.T.);
#8383=FACE_OUTER_BOUND('',#10104,.T.);
#8384=FACE_OUTER_BOUND('',#10105,.T.);
#8385=FACE_OUTER_BOUND('',#10106,.T.);
#8386=FACE_OUTER_BOUND('',#10107,.T.);
#8387=FACE_OUTER_BOUND('',#10108,.T.);
#8388=FACE_OUTER_BOUND('',#10109,.T.);
#8389=FACE_OUTER_BOUND('',#10110,.T.);
#8390=FACE_OUTER_BOUND('',#10111,.T.);
#8391=FACE_OUTER_BOUND('',#10112,.T.);
#8392=FACE_OUTER_BOUND('',#10113,.T.);
#8393=FACE_OUTER_BOUND('',#10114,.T.);
#8394=FACE_OUTER_BOUND('',#10115,.T.);
#8395=FACE_OUTER_BOUND('',#10116,.T.);
#8396=FACE_OUTER_BOUND('',#10118,.T.);
#10077=EDGE_LOOP('',(#25374,#25375,#25376,#25377));
#10078=EDGE_LOOP('',(#25378,#25379,#25380,#25381));
#10079=EDGE_LOOP('',(#25382,#25383,#25384,#25385));
#10080=EDGE_LOOP('',(#25386,#25387,#25388,#25389));
#10081=EDGE_LOOP('',(#25390,#25391,#25392,#25393));
#10082=EDGE_LOOP('',(#25394,#25395,#25396,#25397));
#10083=EDGE_LOOP('',(#25398,#25399,#25400,#25401));
#10084=EDGE_LOOP('',(#25402,#25403,#25404,#25405));
#10085=EDGE_LOOP('',(#25406,#25407,#25408,#25409));
#10086=EDGE_LOOP('',(#25410,#25411,#25412,#25413));
#10087=EDGE_LOOP('',(#25414,#25415,#25416,#25417));
#10088=EDGE_LOOP('',(#25418,#25419,#25420,#25421));
#10089=EDGE_LOOP('',(#25422,#25423,#25424,#25425,#25426));
#10090=EDGE_LOOP('',(#25427,#25428,#25429,#25430));
#10091=EDGE_LOOP('',(#25431,#25432,#25433,#25434));
#10092=EDGE_LOOP('',(#25435,#25436,#25437,#25438));
#10093=EDGE_LOOP('',(#25439,#25440,#25441,#25442));
#10094=EDGE_LOOP('',(#25443,#25444,#25445,#25446));
#10095=EDGE_LOOP('',(#25447,#25448,#25449,#25450));
#10096=EDGE_LOOP('',(#25451,#25452,#25453,#25454));
#10097=EDGE_LOOP('',(#25455,#25456,#25457,#25458));
#10098=EDGE_LOOP('',(#25459,#25460,#25461,#25462));
#10099=EDGE_LOOP('',(#25463,#25464,#25465,#25466));
#10100=EDGE_LOOP('',(#25467,#25468,#25469,#25470));
#10101=EDGE_LOOP('',(#25471,#25472,#25473,#25474));
#10102=EDGE_LOOP('',(#25475,#25476,#25477,#25478,#25479,#25480,#25481,#25482,
#25483,#25484,#25485,#25486,#25487,#25488,#25489,#25490,#25491,#25492,#25493,
#25494,#25495,#25496,#25497,#25498,#25499,#25500,#25501,#25502,#25503));
#10103=EDGE_LOOP('',(#25504,#25505,#25506,#25507,#25508));
#10104=EDGE_LOOP('',(#25509,#25510,#25511,#25512));
#10105=EDGE_LOOP('',(#25513,#25514,#25515,#25516,#25517,#25518,#25519,#25520,
#25521,#25522,#25523,#25524,#25525,#25526,#25527,#25528,#25529,#25530,#25531,
#25532,#25533,#25534,#25535,#25536,#25537,#25538,#25539,#25540));
#10106=EDGE_LOOP('',(#25541,#25542,#25543,#25544));
#10107=EDGE_LOOP('',(#25545,#25546,#25547,#25548));
#10108=EDGE_LOOP('',(#25549,#25550,#25551,#25552));
#10109=EDGE_LOOP('',(#25553,#25554,#25555,#25556));
#10110=EDGE_LOOP('',(#25557,#25558,#25559,#25560));
#10111=EDGE_LOOP('',(#25561,#25562,#25563,#25564));
#10112=EDGE_LOOP('',(#25565,#25566,#25567,#25568,#25569,#25570));
#10113=EDGE_LOOP('',(#25571));
#10114=EDGE_LOOP('',(#25572,#25573,#25574,#25575,#25576,#25577));
#10115=EDGE_LOOP('',(#25578,#25579,#25580));
#10116=EDGE_LOOP('',(#25581));
#10117=EDGE_LOOP('',(#25582,#25583,#25584,#25585,#25586));
#10118=EDGE_LOOP('',(#25587,#25588,#25589,#25590,#25591,#25592,#25593,#25594,
#25595));
#10969=CIRCLE('',#29894,2.4505);
#10970=CIRCLE('',#29907,2.4505);
#10971=CIRCLE('',#29909,1.99475);
#10972=CIRCLE('',#29922,2.4505);
#10973=CIRCLE('',#29923,2.4505);
#10974=CIRCLE('',#29924,1.99475);
#10975=CIRCLE('',#29934,2.2);
#10976=CIRCLE('',#29937,2.4505);
#10977=CIRCLE('',#29939,4.75);
#11399=B_SPLINE_CURVE_WITH_KNOTS('',3,(#53623,#53624,#53625,#53626,#53627,
#53628,#53629,#53630,#53631,#53632),.UNSPECIFIED.,.F.,.F.,(4,3,3,4),(-4.09157007060748,
-3.98172109321816,-2.98629081991362,-2.06659765062439),.UNSPECIFIED.);
#11400=B_SPLINE_CURVE_WITH_KNOTS('',3,(#53635,#53636,#53637,#53638,#53639,
#53640,#53641),.UNSPECIFIED.,.F.,.F.,(4,3,4),(0.,0.995430273304535,1.11662023360662),
 .UNSPECIFIED.);
#11401=B_SPLINE_CURVE_WITH_KNOTS('',3,(#53646,#53647,#53648,#53649,#53650,
#53651,#53652,#53653,#53654,#53655,#53656,#53657,#53658,#53659,#53660,#53661,
#53662,#53663,#53664,#53665,#53666,#53667),.UNSPECIFIED.,.F.,.F.,(4,3,3,
3,3,3,3,4),(-10.3747553777871,-9.95430273304539,-8.95887245974085,-7.96344218643631,
-6.96801191313177,-5.97258163982723,-4.9771513665227,-4.09157007060748),
 .UNSPECIFIED.);
#11402=B_SPLINE_CURVE_WITH_KNOTS('',3,(#53668,#53669,#53670,#53671,#53672,
#53673,#53674,#53675,#53676,#53677,#53678,#53679,#53680,#53681,#53682,#53683,
#53684,#53685,#53686,#53687,#53688,#53689),.UNSPECIFIED.,.F.,.F.,(4,3,3,
3,3,3,3,4),(1.11662023360662,1.99086054660907,2.98629081991362,3.98172109321816,
4.9771513665227,5.97258163982724,6.96801191313178,7.39980554078621),
 .UNSPECIFIED.);
#11403=B_SPLINE_CURVE_WITH_KNOTS('',3,(#53694,#53695,#53696,#53697,#53698,
#53699,#53700,#53701,#53702,#53703,#53704,#53705,#53706,#53707,#53708,#53709,
#53710,#53711,#53712,#53713,#53714,#53715),.UNSPECIFIED.,.F.,.F.,(4,3,3,
3,3,3,3,4),(-16.6579406849666,-15.9268843728726,-14.9314540995681,-13.9360238262635,
-12.940593552959,-11.9451632796545,-10.9497330063499,-10.3747553777871),
 .UNSPECIFIED.);
#11404=B_SPLINE_CURVE_WITH_KNOTS('',3,(#53716,#53717,#53718,#53719,#53720,
#53721,#53722,#53723,#53724,#53725,#53726,#53727,#53728,#53729,#53730,#53731,
#53732,#53733,#53734,#53735,#53736,#53737),.UNSPECIFIED.,.F.,.F.,(4,3,3,
3,3,3,3,4),(7.39980554078621,7.96344218643632,8.95887245974086,9.9543027330454,
10.9497330063499,11.9451632796545,12.940593552959,13.6829908479658),
 .UNSPECIFIED.);
#11405=B_SPLINE_CURVE_WITH_KNOTS('',3,(#53742,#53743,#53744,#53745,#53746,
#53747,#53748,#53749,#53750,#53751,#53752,#53753,#53754,#53755,#53756,#53757,
#53758,#53759,#53760,#53761,#53762,#53763,#53764,#53765,#53766),
 .UNSPECIFIED.,.F.,.F.,(4,3,3,3,3,3,3,3,4),(-22.9411259921462,-22.8948962860044,
-21.8994660126999,-20.9040357393953,-19.9086054660908,-18.9131751927862,
-17.9177449194817,-16.9223146461772,-16.6579406849666),.UNSPECIFIED.);
#11406=B_SPLINE_CURVE_WITH_KNOTS('',3,(#53767,#53768,#53769,#53770,#53771,
#53772,#53773,#53774,#53775,#53776,#53777,#53778,#53779,#53780,#53781,#53782,
#53783,#53784,#53785,#53786,#53787,#53788,#53789,#53790,#53791),
 .UNSPECIFIED.,.F.,.F.,(4,3,3,3,3,3,3,3,4),(13.6829908479658,13.9360238262635,
14.9314540995681,15.9268843728726,16.9223146461772,17.9177449194817,18.9131751927862,
19.9086054660908,19.9661761551454),.UNSPECIFIED.);
#11407=B_SPLINE_CURVE_WITH_KNOTS('',3,(#53796,#53797,#53798,#53799,#53800,
#53801,#53802,#53803,#53804,#53805,#53806,#53807,#53808,#53809,#53810,#53811,
#53812,#53813,#53814,#53815,#53816,#53817),.UNSPECIFIED.,.F.,.F.,(4,3,3,
3,3,3,3,4),(-29.2243112993258,-28.8674779258316,-27.8720476525271,-26.8766173792226,
-25.881187105918,-24.8857568326135,-23.8903265593089,-22.9411259921462),
 .UNSPECIFIED.);
#11408=B_SPLINE_CURVE_WITH_KNOTS('',3,(#53818,#53819,#53820,#53821,#53822,
#53823,#53824,#53825,#53826,#53827,#53828,#53829,#53830,#53831,#53832,#53833,
#53834,#53835,#53836,#53837,#53838,#53839),.UNSPECIFIED.,.F.,.F.,(4,3,3,
3,3,3,3,4),(19.9661761551454,20.9040357393953,21.8994660126999,22.8948962860044,
23.8903265593089,24.8857568326135,25.881187105918,26.249361462325),
 .UNSPECIFIED.);
#11409=B_SPLINE_CURVE_WITH_KNOTS('',3,(#53844,#53845,#53846,#53847,#53848,
#53849,#53850,#53851,#53852,#53853,#53854,#53855,#53856,#53857,#53858,#53859,
#53860,#53861,#53862,#53863,#53864,#53865),.UNSPECIFIED.,.F.,.F.,(4,3,3,
3,3,3,3,4),(-35.5074966065054,-34.8400595656589,-33.8446292923543,-32.8491990190498,
-31.8537687457452,-30.8583384724407,-29.8629081991362,-29.2243112993258),
 .UNSPECIFIED.);
#11410=B_SPLINE_CURVE_WITH_KNOTS('',3,(#53866,#53867,#53868,#53869,#53870,
#53871,#53872,#53873,#53874,#53875,#53876,#53877,#53878,#53879,#53880,#53881,
#53882,#53883,#53884,#53885,#53886,#53887),.UNSPECIFIED.,.F.,.F.,(4,3,3,
3,3,3,3,4),(26.249361462325,26.8766173792225,27.8720476525271,28.8674779258316,
29.8629081991362,30.8583384724407,31.8537687457452,32.5325467695045),
 .UNSPECIFIED.);
#11411=B_SPLINE_CURVE_WITH_KNOTS('',3,(#53892,#53893,#53894,#53895,#53896,
#53897,#53898,#53899,#53900,#53901,#53902,#53903,#53904,#53905,#53906,#53907,
#53908,#53909,#53910,#53911,#53912,#53913),.UNSPECIFIED.,.F.,.F.,(4,3,3,
3,3,3,3,4),(-41.790681913685,-40.8126412054861,-39.8172109321816,-38.821780658877,
-37.8263503855725,-36.8309201122679,-35.8354898389634,-35.5074966065054),
 .UNSPECIFIED.);
#11412=B_SPLINE_CURVE_WITH_KNOTS('',3,(#53914,#53915,#53916,#53917,#53918,
#53919,#53920,#53921,#53922,#53923,#53924,#53925,#53926,#53927,#53928,#53929,
#53930,#53931,#53932,#53933,#53934,#53935),.UNSPECIFIED.,.F.,.F.,(4,3,3,
3,3,3,3,4),(32.5325467695045,32.8491990190498,33.8446292923543,34.8400595656589,
35.8354898389634,36.8309201122679,37.8263503855725,38.8157320766841),
 .UNSPECIFIED.);
#11413=B_SPLINE_CURVE_WITH_KNOTS('',3,(#53940,#53941,#53942,#53943,#53944,
#53945,#53946,#53947,#53948,#53949,#53950,#53951,#53952,#53953,#53954,#53955,
#53956,#53957,#53958,#53959,#53960,#53961,#53962,#53963,#53964),
 .UNSPECIFIED.,.F.,.F.,(4,3,3,3,3,3,3,3,4),(-48.0738672208646,-47.7806531186179,
-46.7852228453133,-45.7897925720088,-44.7943622987043,-43.7989320253997,
-42.8035017520952,-41.8080714787906,-41.790681913685),.UNSPECIFIED.);
#11414=B_SPLINE_CURVE_WITH_KNOTS('',3,(#53965,#53966,#53967,#53968,#53969,
#53970,#53971,#53972,#53973,#53974,#53975,#53976,#53977,#53978,#53979,#53980,
#53981,#53982,#53983,#53984,#53985,#53986,#53987,#53988,#53989),
 .UNSPECIFIED.,.F.,.F.,(4,3,3,3,3,3,3,3,4),(38.8157320766841,38.821780658877,
39.8172109321815,40.8126412054861,41.8080714787906,42.8035017520952,43.7989320253997,
44.7943622987042,45.0989173838637),.UNSPECIFIED.);
#11415=B_SPLINE_CURVE_WITH_KNOTS('',3,(#53994,#53995,#53996,#53997,#53998,
#53999,#54000,#54001,#54002,#54003,#54004,#54005,#54006,#54007,#54008,#54009,
#54010,#54011,#54012,#54013,#54014,#54015),.UNSPECIFIED.,.F.,.F.,(4,3,3,
3,3,3,3,4),(-54.3570525280442,-53.7532347584451,-52.7578044851406,-51.762374211836,
-50.7669439385315,-49.771513665227,-48.7760833919224,-48.0738672208646),
 .UNSPECIFIED.);
#11416=B_SPLINE_CURVE_WITH_KNOTS('',3,(#54016,#54017,#54018,#54019,#54020,
#54021,#54022,#54023,#54024,#54025,#54026,#54027,#54028,#54029,#54030,#54031,
#54032,#54033,#54034,#54035,#54036,#54037),.UNSPECIFIED.,.F.,.F.,(4,3,3,
3,3,3,3,4),(45.0989173838637,45.7897925720088,46.7852228453133,47.7806531186179,
48.7760833919224,49.7715136652269,50.7669439385315,51.3821026910433),
 .UNSPECIFIED.);
#11417=B_SPLINE_CURVE_WITH_KNOTS('',3,(#54042,#54043,#54044,#54045,#54046,
#54047,#54048,#54049,#54050,#54051,#54052,#54053,#54054,#54055,#54056,#54057,
#54058,#54059,#54060,#54061,#54062,#54063),.UNSPECIFIED.,.F.,.F.,(4,3,3,
3,3,3,3,4),(-60.6402378352238,-59.7258163982724,-58.7303861249678,-57.7349558516633,
-56.7395255783587,-55.7440953050542,-54.7486650317496,-54.3570525280442),
 .UNSPECIFIED.);
#11418=B_SPLINE_CURVE_WITH_KNOTS('',3,(#54064,#54065,#54066,#54067,#54068,
#54069,#54070,#54071,#54072,#54073,#54074,#54075,#54076,#54077,#54078,#54079,
#54080,#54081,#54082,#54083,#54084,#54085),.UNSPECIFIED.,.F.,.F.,(4,3,3,
3,3,3,3,4),(51.3821026910433,51.762374211836,52.7578044851406,53.7532347584451,
54.7486650317496,55.7440953050542,56.7395255783587,57.6652879982229),
 .UNSPECIFIED.);
#11419=B_SPLINE_CURVE_WITH_KNOTS('',3,(#54090,#54091,#54092,#54093,#54094,
#54095,#54096,#54097,#54098,#54099,#54100,#54101,#54102,#54103,#54104,#54105,
#54106,#54107,#54108,#54109,#54110,#54111,#54112,#54113,#54114),
 .UNSPECIFIED.,.F.,.F.,(4,3,3,3,3,3,3,3,4),(-66.9234231424034,-66.6938283114041,
-65.6983980380996,-64.702967764795,-63.7075374914905,-62.712107218186,-61.7166769448814,
-60.7212466715769,-60.6402378352238),.UNSPECIFIED.);
#11420=B_SPLINE_CURVE_WITH_KNOTS('',3,(#54115,#54116,#54117,#54118,#54119,
#54120,#54121,#54122,#54123,#54124,#54125,#54126,#54127,#54128,#54129,#54130,
#54131,#54132,#54133,#54134,#54135,#54136,#54137,#54138,#54139),
 .UNSPECIFIED.,.F.,.F.,(4,3,3,3,3,3,3,3,4),(57.6652879982229,57.7349558516632,
58.7303861249678,59.7258163982723,60.7212466715769,61.7166769448814,62.712107218186,
63.7075374914905,63.9484733054025),.UNSPECIFIED.);
#11421=B_SPLINE_CURVE_WITH_KNOTS('',3,(#54144,#54145,#54146,#54147,#54148,
#54149,#54150,#54151,#54152,#54153,#54154,#54155,#54156,#54157,#54158,#54159,
#54160,#54161,#54162,#54163,#54164,#54165),.UNSPECIFIED.,.F.,.F.,(4,3,3,
3,3,3,3,4),(-73.206608449583,-72.6664099512313,-71.6709796779268,-70.6755494046223,
-69.6801191313177,-68.6846888580132,-67.6892585847087,-66.9234231424034),
 .UNSPECIFIED.);
#11422=B_SPLINE_CURVE_WITH_KNOTS('',3,(#54166,#54167,#54168,#54169,#54170,
#54171,#54172,#54173,#54174,#54175,#54176,#54177,#54178,#54179,#54180,#54181,
#54182,#54183,#54184,#54185,#54186,#54187),.UNSPECIFIED.,.F.,.F.,(4,3,3,
3,3,3,3,4),(63.9484733054025,64.702967764795,65.6983980380996,66.6938283114041,
67.6892585847086,68.6846888580132,69.6801191313178,70.2316586125821),
 .UNSPECIFIED.);
#11423=B_SPLINE_CURVE_WITH_KNOTS('',3,(#54194,#54195,#54196,#54197,#54198,
#54199,#54200,#54201,#54202,#54203,#54204,#54205,#54206,#54207,#54208,#54209,
#54210,#54211,#54212),.UNSPECIFIED.,.F.,.F.,(4,3,3,3,3,3,4),(-78.6389915910586,
-77.643561317754,-76.6481310444495,-75.652700771145,-74.6572704978404,-73.6618402245359,
-73.206608449583),.UNSPECIFIED.);
#11424=B_SPLINE_CURVE_WITH_KNOTS('',3,(#54213,#54214,#54215,#54216,#54217,
#54218,#54219,#54220,#54221,#54222,#54223,#54224,#54225,#54226,#54227,#54228,
#54229,#54230,#54231,#54232,#54233,#54234),.UNSPECIFIED.,.F.,.F.,(4,3,3,
3,3,3,3,4),(70.2316586125821,70.6755494046223,71.6709796779268,72.6664099512313,
73.6618402245359,74.6572704978404,75.6527007711449,76.5148439197617),
 .UNSPECIFIED.);
#11425=B_SPLINE_CURVE_WITH_KNOTS('',3,(#54240,#54241,#54242,#54243,#54244,
#54245,#54246),.UNSPECIFIED.,.F.,.F.,(4,1,1,1,4),(84.8230016469244,85.2782334218773,
86.2736636951819,87.2690939684864,88.1887871377756),.UNSPECIFIED.);
#11426=B_SPLINE_CURVE_WITH_KNOTS('',3,(#54249,#54250,#54251,#54252,#54253,
#54254),.UNSPECIFIED.,.F.,.F.,(4,1,1,4),(84.8230016469244,84.9562887716121,
85.9517190449167,86.9471493182212),.UNSPECIFIED.);
#11427=B_SPLINE_CURVE_WITH_KNOTS('',3,(#54259,#54260,#54261,#54262,#54263,
#54264,#54265,#54266,#54267,#54268),.UNSPECIFIED.,.F.,.F.,(4,1,1,1,1,1,
1,4),(78.5398163397448,79.3056517820501,80.3010820553546,81.2965123286592,
82.2919426019637,83.2873728752682,84.2828031485728,84.8230016469244),
 .UNSPECIFIED.);
#11428=B_SPLINE_CURVE_WITH_KNOTS('',3,(#54269,#54270,#54271,#54272,#54273,
#54274,#54275,#54276,#54277,#54278),.UNSPECIFIED.,.F.,.F.,(4,1,1,1,1,1,
1,4),(78.5398163397448,78.9837071317849,79.9791374050894,80.974567678394,
81.9699979516985,82.9654282250031,83.9608584983076,84.8230016469244),
 .UNSPECIFIED.);
#11429=B_SPLINE_CURVE_WITH_KNOTS('',3,(#54283,#54284,#54285,#54286,#54287,
#54288,#54289,#54290,#54291,#54292,#54293),.UNSPECIFIED.,.F.,.F.,(4,1,1,
1,1,1,1,1,4),(72.2566310325652,72.3376398689183,73.3330701422229,74.3285004155274,
75.3239306888319,76.3193609621365,77.314791235441,78.3102215087456,78.5398163397448),
 .UNSPECIFIED.);
#11430=B_SPLINE_CURVE_WITH_KNOTS('',3,(#54294,#54295,#54296,#54297,#54298,
#54299,#54300,#54301,#54302,#54303),.UNSPECIFIED.,.F.,.F.,(4,1,1,1,1,1,
1,4),(72.2566310325652,73.0111254919577,74.0065557652622,75.0019860385667,
75.9974163118713,76.9928465851758,77.9882768584804,78.5398163397448),
 .UNSPECIFIED.);
#11431=B_SPLINE_CURVE_WITH_KNOTS('',3,(#54308,#54309,#54310,#54311,#54312,
#54313,#54314,#54315,#54316,#54317),.UNSPECIFIED.,.F.,.F.,(4,1,1,1,1,1,
1,4),(65.9734457253856,66.3650582290911,67.3604885023956,68.3559187757002,
69.3513490490047,70.3467793223092,71.3422095956138,72.2566310325652),
 .UNSPECIFIED.);
#11432=B_SPLINE_CURVE_WITH_KNOTS('',3,(#54318,#54319,#54320,#54321,#54322,
#54323,#54324,#54325,#54326,#54327,#54328),.UNSPECIFIED.,.F.,.F.,(4,1,1,
1,1,1,1,1,4),(65.9734457253856,66.0431135788259,67.0385438521304,68.033974125435,
69.0294043987395,70.0248346720441,71.0202649453486,72.0156952186531,72.2566310325652),
 .UNSPECIFIED.);
#11433=B_SPLINE_CURVE_WITH_KNOTS('',3,(#54333,#54334,#54335,#54336,#54337,
#54338,#54339,#54340,#54341,#54342),.UNSPECIFIED.,.F.,.F.,(4,1,1,1,1,1,
1,4),(59.6902604182061,60.3924765892639,61.3879068625684,62.3833371358729,
63.3787674091775,64.374197682482,65.3696279557865,65.9734457253856),
 .UNSPECIFIED.);
#11434=B_SPLINE_CURVE_WITH_KNOTS('',3,(#54343,#54344,#54345,#54346,#54347,
#54348,#54349,#54350,#54351,#54352),.UNSPECIFIED.,.F.,.F.,(4,1,1,1,1,1,
1,4),(59.690260418206,60.0705319389987,61.0659622123032,62.0613924856077,
63.0568227589123,64.0522530322168,65.0476833055214,65.9734457253856),
 .UNSPECIFIED.);
#11435=B_SPLINE_CURVE_WITH_KNOTS('',3,(#54357,#54358,#54359,#54360,#54361,
#54362,#54363,#54364,#54365,#54366,#54367),.UNSPECIFIED.,.F.,.F.,(4,1,1,
1,1,1,1,1,4),(53.4070751110265,53.4244646761321,54.4198949494366,55.4153252227412,
56.4107554960457,57.4061857693502,58.4016160426548,59.3970463159593,59.6902604182061),
 .UNSPECIFIED.);
#11436=B_SPLINE_CURVE_WITH_KNOTS('',3,(#54368,#54369,#54370,#54371,#54372,
#54373,#54374,#54375,#54376,#54377),.UNSPECIFIED.,.F.,.F.,(4,1,1,1,1,1,
1,4),(53.4070751110264,54.0979502991714,55.093380572476,56.0888108457805,
57.084241119085,58.0796713923896,59.0751016656941,59.690260418206),
 .UNSPECIFIED.);
#11437=B_SPLINE_CURVE_WITH_KNOTS('',3,(#54382,#54383,#54384,#54385,#54386,
#54387,#54388,#54389,#54390,#54391),.UNSPECIFIED.,.F.,.F.,(4,1,1,1,1,1,
1,4),(47.1238898038469,47.4518830363048,48.4473133096094,49.4427435829139,
50.4381738562185,51.433604129523,52.4290344028275,53.4070751110265),
 .UNSPECIFIED.);
#11438=B_SPLINE_CURVE_WITH_KNOTS('',3,(#54392,#54393,#54394,#54395,#54396,
#54397,#54398,#54399,#54400,#54401,#54402),.UNSPECIFIED.,.F.,.F.,(4,1,1,
1,1,1,1,1,4),(47.1238898038468,47.1299383860397,48.1253686593442,49.1207989326487,
50.1162292059533,51.1116594792578,52.1070897525623,53.1025200258669,53.4070751110264),
 .UNSPECIFIED.);
#11439=B_SPLINE_CURVE_WITH_KNOTS('',3,(#54407,#54408,#54409,#54410,#54411,
#54412,#54413,#54414,#54415,#54416),.UNSPECIFIED.,.F.,.F.,(4,1,1,1,1,1,
1,4),(40.8407044966673,41.4793013964776,42.4747316697821,43.4701619430867,
44.4655922163912,45.4610224896958,46.4564527630003,47.1238898038469),
 .UNSPECIFIED.);
#11440=B_SPLINE_CURVE_WITH_KNOTS('',3,(#54417,#54418,#54419,#54420,#54421,
#54422,#54423,#54424,#54425,#54426),.UNSPECIFIED.,.F.,.F.,(4,1,1,1,1,1,
1,4),(40.8407044966673,41.1573567462124,42.152787019517,43.1482172928215,
44.143647566126,45.1390778394306,46.1345081127351,47.1238898038468),
 .UNSPECIFIED.);
#11441=B_SPLINE_CURVE_WITH_KNOTS('',3,(#54431,#54432,#54433,#54434,#54435,
#54436,#54437,#54438,#54439,#54440),.UNSPECIFIED.,.F.,.F.,(4,1,1,1,1,1,
1,4),(34.5575191894877,35.5067197566504,36.5021500299549,37.4975803032595,
38.493010576564,39.4884408498685,40.4838711231731,40.8407044966673),
 .UNSPECIFIED.);
#11442=B_SPLINE_CURVE_WITH_KNOTS('',3,(#54441,#54442,#54443,#54444,#54445,
#54446,#54447,#54448,#54449,#54450),.UNSPECIFIED.,.F.,.F.,(4,1,1,1,1,1,
1,4),(34.5575191894877,35.1847751063852,36.1802053796897,37.1756356529943,
38.1710659262988,39.1664961996033,40.1619264729079,40.8407044966673),
 .UNSPECIFIED.);
#11443=B_SPLINE_CURVE_WITH_KNOTS('',3,(#54455,#54456,#54457,#54458,#54459,
#54460,#54461,#54462,#54463,#54464,#54465),.UNSPECIFIED.,.F.,.F.,(4,1,1,
1,1,1,1,1,4),(28.2743338823081,28.5387078435186,29.5341381168231,30.5295683901277,
31.5249986634322,32.5204289367368,33.5158592100413,34.5112894833458,34.5575191894877),
 .UNSPECIFIED.);
#11444=B_SPLINE_CURVE_WITH_KNOTS('',3,(#54466,#54467,#54468,#54469,#54470,
#54471,#54472,#54473,#54474,#54475),.UNSPECIFIED.,.F.,.F.,(4,1,1,1,1,1,
1,4),(28.2743338823081,29.212193466558,30.2076237398625,31.203054013167,
32.1984842864716,33.1939145597761,34.1893448330807,34.5575191894877),
 .UNSPECIFIED.);
#11445=B_SPLINE_CURVE_WITH_KNOTS('',3,(#54480,#54481,#54482,#54483,#54484,
#54485,#54486,#54487,#54488,#54489),.UNSPECIFIED.,.F.,.F.,(4,1,1,1,1,1,
1,4),(21.9911485751285,22.5661262036914,23.5615564769959,24.5569867503004,
25.552417023605,26.5478472969095,27.5432775702141,28.2743338823081),
 .UNSPECIFIED.);
#11446=B_SPLINE_CURVE_WITH_KNOTS('',3,(#54490,#54491,#54492,#54493,#54494,
#54495,#54496,#54497,#54498,#54499,#54500),.UNSPECIFIED.,.F.,.F.,(4,1,1,
1,1,1,1,1,4),(21.9911485751285,22.2441815534262,23.2396118267307,24.2350421000353,
25.2304723733398,26.2259026466443,27.2213329199489,28.2167631932534,28.2743338823081),
 .UNSPECIFIED.);
#11447=B_SPLINE_CURVE_WITH_KNOTS('',3,(#54505,#54506,#54507,#54508,#54509,
#54510,#54511,#54512,#54513,#54514),.UNSPECIFIED.,.F.,.F.,(4,1,1,1,1,1,
1,4),(15.7079632679489,16.5935445638641,17.5889748371687,18.5844051104732,
19.5798353837777,20.5752656570823,21.5706959303868,21.9911485751285),
 .UNSPECIFIED.);
#11448=B_SPLINE_CURVE_WITH_KNOTS('',3,(#54515,#54516,#54517,#54518,#54519,
#54520,#54521,#54522,#54523,#54524),.UNSPECIFIED.,.F.,.F.,(4,1,1,1,1,1,
1,4),(15.7079632679489,16.271599913599,17.2670301869035,18.262460460208,
19.2578907335126,20.2533210068171,21.2487512801216,21.9911485751285),
 .UNSPECIFIED.);
#11449=B_SPLINE_CURVE_WITH_KNOTS('',3,(#54854,#54855,#54856,#54857,#54858,
#54859,#54860,#54861,#54862,#54863,#54864,#54865,#54866,#54867,#54868,#54869,
#54870,#54871,#54872,#54873,#54874,#54875,#54876,#54877,#54878,#54879,#54880,
#54881,#54882,#54883,#54884,#54885,#54886,#54887,#54888,#54889,#54890,#54891,
#54892,#54893,#54894,#54895,#54896,#54897,#54898,#54899,#54900,#54901,#54902,
#54903,#54904,#54905,#54906,#54907,#54908,#54909,#54910,#54911,#54912,#54913,
#54914,#54915,#54916,#54917,#54918,#54919,#54920,#54921,#54922,#54923,#54924,
#54925,#54926,#54927,#54928,#54929,#54930,#54931,#54932,#54933,#54934,#54935,
#54936,#54937,#54938),.UNSPECIFIED.,.F.,.F.,(4,3,3,3,3,3,3,3,3,3,3,3,3,
3,3,3,3,3,3,3,3,3,3,3,3,3,3,3,4),(-0.46178896489977,-0.443269576631881,
-0.417631722778642,-0.404721877370092,-0.398764222638072,-0.394155820681543,
-0.368772666244105,-0.349060357493822,-0.339629635278542,-0.335643839010919,
-0.310878151516634,-0.285927162697937,-0.262162840527267,-0.247926297736166,
-0.244191128511931,-0.22070382990977,-0.211074196241844,-0.187109670400446,
-0.16372096160039,-0.158787676279632,-0.135433515521448,-0.112095499914898,
-0.0891458125607591,-0.0803315743918779,-0.0766175656125797,-0.0541537985024097,
-0.0320532662641283,-0.0106598536043234,0.),.UNSPECIFIED.);
#11450=B_SPLINE_CURVE_WITH_KNOTS('',3,(#54939,#54940,#54941,#54942),
 .UNSPECIFIED.,.F.,.F.,(4,4),(76.5148439197617,76.5723939404342),
 .UNSPECIFIED.);
#11451=B_SPLINE_CURVE_WITH_KNOTS('',3,(#54944,#54945,#54946,#54947,#54948,
#54949,#54950,#54951,#54952,#54953,#54954,#54955,#54956,#54957,#54958,#54959,
#54960,#54961,#54962,#54963,#54964,#54965,#54966,#54967,#54968,#54969,#54970,
#54971,#54972,#54973,#54974,#54975,#54976,#54977,#54978,#54979,#54980,#54981,
#54982,#54983,#54984,#54985,#54986,#54987,#54988,#54989,#54990,#54991,#54992,
#54993,#54994,#54995,#54996,#54997,#54998,#54999,#55000,#55001,#55002,#55003,
#55004,#55005,#55006,#55007,#55008,#55009,#55010,#55011,#55012,#55013,#55014,
#55015,#55016,#55017,#55018,#55019,#55020,#55021,#55022,#55023,#55024,#55025,
#55026,#55027,#55028),.UNSPECIFIED.,.F.,.F.,(4,3,3,3,3,3,3,3,3,3,3,3,3,
3,3,3,3,3,3,3,3,3,3,3,3,3,3,3,4),(-0.463803050843718,-0.448467893697323,
-0.426743397417581,-0.414223922938524,-0.409751274283662,-0.387170225743088,
-0.368152587837341,-0.359003292171437,-0.354824498455266,-0.331563035795037,
-0.307429557470556,-0.289329448727194,-0.275754367169673,-0.271732612569561,
-0.267646445348118,-0.243218974605062,-0.23502912249711,-0.211434740552809,
-0.187352387065262,-0.181481954926502,-0.157053292656267,-0.132137985018908,
-0.107029339777651,-0.0963678781398328,-0.09101691238576,-0.0652788128183591,
-0.0394985536882287,-0.0142609901943899,0.),.UNSPECIFIED.);
#11452=B_SPLINE_CURVE_WITH_KNOTS('',3,(#55029,#55030,#55031,#55032,#55033,
#55034,#55035,#55036,#55037),.UNSPECIFIED.,.F.,.F.,(4,1,1,1,1,1,4),(10.374755377787,
11.2944485470763,12.2898788203808,13.2853090936853,14.2807393669899,15.2761696402944,
15.7079632679489),.UNSPECIFIED.);
#11453=B_SPLINE_CURVE_WITH_KNOTS('',3,(#55043,#55044,#55045,#55046,#55047,
#55048,#55049,#55050,#55051,#55052,#55053,#55054,#55055,#55056,#55057,#55058,
#55059,#55060,#55061,#55062,#55063,#55064,#55065,#55066,#55067,#55068,#55069,
#55070,#55071,#55072,#55073,#55074,#55075,#55076,#55077,#55078,#55079,#55080,
#55081,#55082,#55083,#55084,#55085,#55086,#55087,#55088,#55089,#55090,#55091,
#55092,#55093,#55094,#55095,#55096,#55097,#55098,#55099,#55100,#55101,#55102,
#55103,#55104,#55105,#55106,#55107,#55108,#55109,#55110,#55111,#55112,#55113,
#55114,#55115,#55116,#55117,#55118,#55119,#55120,#55121,#55122,#55123,#55124,
#55125,#55126,#55127),.UNSPECIFIED.,.F.,.F.,(4,3,3,3,3,3,3,3,3,3,3,3,3,
3,3,3,3,3,3,3,3,3,3,3,3,3,3,3,4),(-0.461788964899772,-0.44326957663188,
-0.417631722122037,-0.404721876754524,-0.398764200476566,-0.394155769220187,
-0.368772614542353,-0.349060312254788,-0.339629567665009,-0.335643823398429,
-0.31087813518458,-0.285927150448892,-0.262162811144695,-0.247926244119766,
-0.244191073680388,-0.220703763308337,-0.211074196241828,-0.187109662130682,
-0.163720954364347,-0.158787676781602,-0.135433511432081,-0.112095502700825,
-0.0891458325698699,-0.0803315769099513,-0.0766175669273989,-0.0541538125628121,
-0.0320532998196413,-0.0106599118168654,0.),.UNSPECIFIED.);
#11454=B_SPLINE_CURVE_WITH_KNOTS('',3,(#55130,#55131,#55132,#55133,#55134,
#55135,#55136,#55137),.UNSPECIFIED.,.F.,.F.,(4,1,1,1,1,4),(11.6163931973414,
12.611823470646,13.6072537439505,14.6026840172551,15.5981142905596,15.7079632679489),
 .UNSPECIFIED.);
#11455=B_SPLINE_CURVE_WITH_KNOTS('',3,(#55466,#55467,#55468,#55469,#55470,
#55471,#55472,#55473,#55474,#55475,#55476,#55477,#55478,#55479,#55480,#55481,
#55482,#55483,#55484,#55485,#55486,#55487,#55488,#55489,#55490,#55491,#55492,
#55493,#55494,#55495,#55496,#55497,#55498,#55499,#55500,#55501,#55502,#55503,
#55504,#55505,#55506,#55507,#55508,#55509,#55510,#55511,#55512,#55513,#55514,
#55515,#55516,#55517,#55518,#55519,#55520,#55521,#55522,#55523,#55524,#55525,
#55526,#55527,#55528,#55529,#55530,#55531,#55532,#55533,#55534,#55535,#55536,
#55537,#55538,#55539,#55540,#55541,#55542,#55543,#55544,#55545,#55546,#55547,
#55548,#55549,#55550),.UNSPECIFIED.,.F.,.F.,(4,3,3,3,3,3,3,3,3,3,3,3,3,
3,3,3,3,3,3,3,3,3,3,3,3,3,3,3,4),(-0.463803050843723,-0.448467893697328,
-0.42674338256529,-0.414223896421318,-0.409751265194179,-0.387170206067839,
-0.368152570621498,-0.359003265127981,-0.354824456856625,-0.331562984878854,
-0.307429519283418,-0.28932942008684,-0.275754345689407,-0.271732471107105,
-0.267646412172009,-0.243218942153542,-0.235029122497107,-0.211434734441675,
-0.187352373722984,-0.181481960030832,-0.157053290808756,-0.132137976349438,
-0.107029329959023,-0.096367863765101,-0.0910169135905318,-0.0652788097838639,
-0.039498554230681,-0.0142610096161325,0.),.UNSPECIFIED.);
#11456=B_SPLINE_CURVE_WITH_KNOTS('',3,(#55554,#55555,#55556,#55557,#55558,
#55559),.UNSPECIFIED.,.F.,.F.,(4,2,4),(1.2907552072404,1.37375394746467,
1.45675268768893),.UNSPECIFIED.);
#11457=B_SPLINE_CURVE_WITH_KNOTS('',3,(#55567,#55568,#55569,#55570,#55571,
#55572),.UNSPECIFIED.,.F.,.F.,(4,2,4),(1.2907552072404,1.37375394746467,
1.45675268768893),.UNSPECIFIED.);
#11458=B_SPLINE_CURVE_WITH_KNOTS('',3,(#55578,#55579,#55580,#55581,#55582,
#55583),.UNSPECIFIED.,.F.,.F.,(4,2,4),(1.2907552072404,1.37375394746467,
1.45675268768893),.UNSPECIFIED.);
#11459=B_SPLINE_CURVE_WITH_KNOTS('',3,(#55589,#55590,#55591,#55592,#55593,
#55594),.UNSPECIFIED.,.F.,.F.,(4,2,4),(1.2907552072404,1.37375394746467,
1.45675268768893),.UNSPECIFIED.);
#11460=B_SPLINE_CURVE_WITH_KNOTS('',3,(#55600,#55601,#55602,#55603,#55604,
#55605),.UNSPECIFIED.,.F.,.F.,(4,2,4),(1.2907552072404,1.37375394746467,
1.45675268768893),.UNSPECIFIED.);
#11461=B_SPLINE_CURVE_WITH_KNOTS('',3,(#55610,#55611,#55612,#55613,#55614,
#55615),.UNSPECIFIED.,.F.,.F.,(4,2,4),(1.2907552072404,1.37375394746467,
1.45675268768893),.UNSPECIFIED.);
#13832=VERTEX_POINT('',#53619);
#13833=VERTEX_POINT('',#53620);
#13834=VERTEX_POINT('',#53622);
#13835=VERTEX_POINT('',#53633);
#13836=VERTEX_POINT('',#53643);
#13837=VERTEX_POINT('',#53644);
#13838=VERTEX_POINT('',#53691);
#13839=VERTEX_POINT('',#53692);
#13840=VERTEX_POINT('',#53739);
#13841=VERTEX_POINT('',#53740);
#13842=VERTEX_POINT('',#53793);
#13843=VERTEX_POINT('',#53794);
#13844=VERTEX_POINT('',#53841);
#13845=VERTEX_POINT('',#53842);
#13846=VERTEX_POINT('',#53889);
#13847=VERTEX_POINT('',#53890);
#13848=VERTEX_POINT('',#53937);
#13849=VERTEX_POINT('',#53938);
#13850=VERTEX_POINT('',#53991);
#13851=VERTEX_POINT('',#53992);
#13852=VERTEX_POINT('',#54039);
#13853=VERTEX_POINT('',#54040);
#13854=VERTEX_POINT('',#54087);
#13855=VERTEX_POINT('',#54088);
#13856=VERTEX_POINT('',#54141);
#13857=VERTEX_POINT('',#54142);
#13858=VERTEX_POINT('',#54189);
#13859=VERTEX_POINT('',#54190);
#13860=VERTEX_POINT('',#54192);
#13861=VERTEX_POINT('',#54236);
#13862=VERTEX_POINT('',#54237);
#13863=VERTEX_POINT('',#54239);
#13864=VERTEX_POINT('',#54247);
#13865=VERTEX_POINT('',#54256);
#13866=VERTEX_POINT('',#54257);
#13867=VERTEX_POINT('',#54280);
#13868=VERTEX_POINT('',#54281);
#13869=VERTEX_POINT('',#54305);
#13870=VERTEX_POINT('',#54306);
#13871=VERTEX_POINT('',#54330);
#13872=VERTEX_POINT('',#54331);
#13873=VERTEX_POINT('',#54354);
#13874=VERTEX_POINT('',#54355);
#13875=VERTEX_POINT('',#54379);
#13876=VERTEX_POINT('',#54380);
#13877=VERTEX_POINT('',#54404);
#13878=VERTEX_POINT('',#54405);
#13879=VERTEX_POINT('',#54428);
#13880=VERTEX_POINT('',#54429);
#13881=VERTEX_POINT('',#54452);
#13882=VERTEX_POINT('',#54453);
#13883=VERTEX_POINT('',#54477);
#13884=VERTEX_POINT('',#54478);
#13885=VERTEX_POINT('',#54502);
#13886=VERTEX_POINT('',#54503);
#13887=VERTEX_POINT('',#54853);
#13888=VERTEX_POINT('',#54943);
#13889=VERTEX_POINT('',#55039);
#13890=VERTEX_POINT('',#55042);
#13891=VERTEX_POINT('',#55552);
#13892=VERTEX_POINT('',#55553);
#13893=VERTEX_POINT('',#55560);
#13894=VERTEX_POINT('',#55562);
#13895=VERTEX_POINT('',#55566);
#13896=VERTEX_POINT('',#55573);
#13897=VERTEX_POINT('',#55577);
#13898=VERTEX_POINT('',#55584);
#13899=VERTEX_POINT('',#55588);
#13900=VERTEX_POINT('',#55595);
#13901=VERTEX_POINT('',#55599);
#13902=VERTEX_POINT('',#55606);
#13903=VERTEX_POINT('',#55619);
#13904=VERTEX_POINT('',#55626);
#17691=EDGE_CURVE('',#13832,#13833,#4091,.T.);
#17692=EDGE_CURVE('',#13832,#13834,#11399,.T.);
#17693=EDGE_CURVE('',#13834,#13835,#10969,.T.);
#17694=EDGE_CURVE('',#13835,#13833,#11400,.T.);
#17695=EDGE_CURVE('',#13836,#13837,#4092,.T.);
#17696=EDGE_CURVE('',#13836,#13832,#11401,.T.);
#17697=EDGE_CURVE('',#13833,#13837,#11402,.T.);
#17698=EDGE_CURVE('',#13838,#13839,#4093,.T.);
#17699=EDGE_CURVE('',#13838,#13836,#11403,.T.);
#17700=EDGE_CURVE('',#13837,#13839,#11404,.T.);
#17701=EDGE_CURVE('',#13840,#13841,#4094,.T.);
#17702=EDGE_CURVE('',#13840,#13838,#11405,.T.);
#17703=EDGE_CURVE('',#13839,#13841,#11406,.T.);
#17704=EDGE_CURVE('',#13842,#13843,#4095,.T.);
#17705=EDGE_CURVE('',#13842,#13840,#11407,.T.);
#17706=EDGE_CURVE('',#13841,#13843,#11408,.T.);
#17707=EDGE_CURVE('',#13844,#13845,#4096,.T.);
#17708=EDGE_CURVE('',#13844,#13842,#11409,.T.);
#17709=EDGE_CURVE('',#13843,#13845,#11410,.T.);
#17710=EDGE_CURVE('',#13846,#13847,#4097,.T.);
#17711=EDGE_CURVE('',#13846,#13844,#11411,.T.);
#17712=EDGE_CURVE('',#13845,#13847,#11412,.T.);
#17713=EDGE_CURVE('',#13848,#13849,#4098,.T.);
#17714=EDGE_CURVE('',#13848,#13846,#11413,.T.);
#17715=EDGE_CURVE('',#13847,#13849,#11414,.T.);
#17716=EDGE_CURVE('',#13850,#13851,#4099,.T.);
#17717=EDGE_CURVE('',#13850,#13848,#11415,.T.);
#17718=EDGE_CURVE('',#13849,#13851,#11416,.T.);
#17719=EDGE_CURVE('',#13852,#13853,#4100,.T.);
#17720=EDGE_CURVE('',#13852,#13850,#11417,.T.);
#17721=EDGE_CURVE('',#13851,#13853,#11418,.T.);
#17722=EDGE_CURVE('',#13854,#13855,#4101,.T.);
#17723=EDGE_CURVE('',#13854,#13852,#11419,.T.);
#17724=EDGE_CURVE('',#13853,#13855,#11420,.T.);
#17725=EDGE_CURVE('',#13856,#13857,#4102,.T.);
#17726=EDGE_CURVE('',#13856,#13854,#11421,.T.);
#17727=EDGE_CURVE('',#13855,#13857,#11422,.T.);
#17728=EDGE_CURVE('',#13858,#13859,#4103,.T.);
#17729=EDGE_CURVE('',#13860,#13858,#10970,.T.);
#17730=EDGE_CURVE('',#13860,#13856,#11423,.T.);
#17731=EDGE_CURVE('',#13857,#13859,#11424,.T.);
#17732=EDGE_CURVE('',#13861,#13862,#4104,.T.);
#17733=EDGE_CURVE('',#13861,#13863,#11425,.T.);
#17734=EDGE_CURVE('',#13864,#13863,#10971,.T.);
#17735=EDGE_CURVE('',#13862,#13864,#11426,.T.);
#17736=EDGE_CURVE('',#13865,#13866,#4105,.T.);
#17737=EDGE_CURVE('',#13865,#13861,#11427,.T.);
#17738=EDGE_CURVE('',#13866,#13862,#11428,.T.);
#17739=EDGE_CURVE('',#13867,#13868,#4106,.T.);
#17740=EDGE_CURVE('',#13867,#13865,#11429,.T.);
#17741=EDGE_CURVE('',#13868,#13866,#11430,.T.);
#17742=EDGE_CURVE('',#13869,#13870,#4107,.T.);
#17743=EDGE_CURVE('',#13869,#13867,#11431,.T.);
#17744=EDGE_CURVE('',#13870,#13868,#11432,.T.);
#17745=EDGE_CURVE('',#13871,#13872,#4108,.T.);
#17746=EDGE_CURVE('',#13871,#13869,#11433,.T.);
#17747=EDGE_CURVE('',#13872,#13870,#11434,.T.);
#17748=EDGE_CURVE('',#13873,#13874,#4109,.T.);
#17749=EDGE_CURVE('',#13873,#13871,#11435,.T.);
#17750=EDGE_CURVE('',#13874,#13872,#11436,.T.);
#17751=EDGE_CURVE('',#13875,#13876,#4110,.T.);
#17752=EDGE_CURVE('',#13875,#13873,#11437,.T.);
#17753=EDGE_CURVE('',#13876,#13874,#11438,.T.);
#17754=EDGE_CURVE('',#13877,#13878,#4111,.T.);
#17755=EDGE_CURVE('',#13877,#13875,#11439,.T.);
#17756=EDGE_CURVE('',#13878,#13876,#11440,.T.);
#17757=EDGE_CURVE('',#13879,#13880,#4112,.T.);
#17758=EDGE_CURVE('',#13879,#13877,#11441,.T.);
#17759=EDGE_CURVE('',#13880,#13878,#11442,.T.);
#17760=EDGE_CURVE('',#13881,#13882,#4113,.T.);
#17761=EDGE_CURVE('',#13881,#13879,#11443,.T.);
#17762=EDGE_CURVE('',#13882,#13880,#11444,.T.);
#17763=EDGE_CURVE('',#13883,#13884,#4114,.T.);
#17764=EDGE_CURVE('',#13883,#13881,#11445,.T.);
#17765=EDGE_CURVE('',#13884,#13882,#11446,.T.);
#17766=EDGE_CURVE('',#13885,#13886,#4115,.T.);
#17767=EDGE_CURVE('',#13885,#13883,#11447,.T.);
#17768=EDGE_CURVE('',#13886,#13884,#11448,.T.);
#17769=EDGE_CURVE('',#13887,#13864,#11449,.T.);
#17770=EDGE_CURVE('',#13859,#13887,#11450,.T.);
#17771=EDGE_CURVE('',#13888,#13835,#11451,.T.);
#17772=EDGE_CURVE('',#13888,#13886,#11452,.T.);
#17773=EDGE_CURVE('',#13835,#13889,#10972,.T.);
#17774=EDGE_CURVE('',#13889,#13834,#10973,.T.);
#17775=EDGE_CURVE('',#13834,#13890,#11453,.T.);
#17776=EDGE_CURVE('',#13890,#13888,#10974,.T.);
#17777=EDGE_CURVE('',#13890,#13885,#11454,.T.);
#17778=EDGE_CURVE('',#13863,#13860,#11455,.T.);
#17779=EDGE_CURVE('',#13891,#13892,#11456,.T.);
#17780=EDGE_CURVE('',#13891,#13893,#4116,.T.);
#17781=EDGE_CURVE('',#13893,#13894,#4117,.T.);
#17782=EDGE_CURVE('',#13892,#13894,#4118,.T.);
#17783=EDGE_CURVE('',#13892,#13895,#11457,.T.);
#17784=EDGE_CURVE('',#13894,#13896,#4119,.T.);
#17785=EDGE_CURVE('',#13895,#13896,#4120,.T.);
#17786=EDGE_CURVE('',#13895,#13897,#11458,.T.);
#17787=EDGE_CURVE('',#13896,#13898,#4121,.T.);
#17788=EDGE_CURVE('',#13897,#13898,#4122,.T.);
#17789=EDGE_CURVE('',#13897,#13899,#11459,.T.);
#17790=EDGE_CURVE('',#13898,#13900,#4123,.T.);
#17791=EDGE_CURVE('',#13899,#13900,#4124,.T.);
#17792=EDGE_CURVE('',#13901,#13891,#11460,.T.);
#17793=EDGE_CURVE('',#13901,#13902,#4125,.T.);
#17794=EDGE_CURVE('',#13902,#13893,#4126,.T.);
#17795=EDGE_CURVE('',#13899,#13901,#11461,.T.);
#17796=EDGE_CURVE('',#13900,#13902,#4127,.T.);
#17797=EDGE_CURVE('',#13903,#13903,#10975,.T.);
#17798=EDGE_CURVE('',#13889,#13903,#4128,.T.);
#17799=EDGE_CURVE('',#13858,#13887,#10976,.T.);
#17800=EDGE_CURVE('',#13904,#13904,#10977,.T.);
#17801=EDGE_CURVE('',#13897,#13904,#196,.T.);
#25374=ORIENTED_EDGE('',*,*,#17691,.F.);
#25375=ORIENTED_EDGE('',*,*,#17692,.T.);
#25376=ORIENTED_EDGE('',*,*,#17693,.T.);
#25377=ORIENTED_EDGE('',*,*,#17694,.T.);
#25378=ORIENTED_EDGE('',*,*,#17695,.F.);
#25379=ORIENTED_EDGE('',*,*,#17696,.T.);
#25380=ORIENTED_EDGE('',*,*,#17691,.T.);
#25381=ORIENTED_EDGE('',*,*,#17697,.T.);
#25382=ORIENTED_EDGE('',*,*,#17698,.F.);
#25383=ORIENTED_EDGE('',*,*,#17699,.T.);
#25384=ORIENTED_EDGE('',*,*,#17695,.T.);
#25385=ORIENTED_EDGE('',*,*,#17700,.T.);
#25386=ORIENTED_EDGE('',*,*,#17701,.F.);
#25387=ORIENTED_EDGE('',*,*,#17702,.T.);
#25388=ORIENTED_EDGE('',*,*,#17698,.T.);
#25389=ORIENTED_EDGE('',*,*,#17703,.T.);
#25390=ORIENTED_EDGE('',*,*,#17704,.F.);
#25391=ORIENTED_EDGE('',*,*,#17705,.T.);
#25392=ORIENTED_EDGE('',*,*,#17701,.T.);
#25393=ORIENTED_EDGE('',*,*,#17706,.T.);
#25394=ORIENTED_EDGE('',*,*,#17707,.F.);
#25395=ORIENTED_EDGE('',*,*,#17708,.T.);
#25396=ORIENTED_EDGE('',*,*,#17704,.T.);
#25397=ORIENTED_EDGE('',*,*,#17709,.T.);
#25398=ORIENTED_EDGE('',*,*,#17710,.F.);
#25399=ORIENTED_EDGE('',*,*,#17711,.T.);
#25400=ORIENTED_EDGE('',*,*,#17707,.T.);
#25401=ORIENTED_EDGE('',*,*,#17712,.T.);
#25402=ORIENTED_EDGE('',*,*,#17713,.F.);
#25403=ORIENTED_EDGE('',*,*,#17714,.T.);
#25404=ORIENTED_EDGE('',*,*,#17710,.T.);
#25405=ORIENTED_EDGE('',*,*,#17715,.T.);
#25406=ORIENTED_EDGE('',*,*,#17716,.F.);
#25407=ORIENTED_EDGE('',*,*,#17717,.T.);
#25408=ORIENTED_EDGE('',*,*,#17713,.T.);
#25409=ORIENTED_EDGE('',*,*,#17718,.T.);
#25410=ORIENTED_EDGE('',*,*,#17719,.F.);
#25411=ORIENTED_EDGE('',*,*,#17720,.T.);
#25412=ORIENTED_EDGE('',*,*,#17716,.T.);
#25413=ORIENTED_EDGE('',*,*,#17721,.T.);
#25414=ORIENTED_EDGE('',*,*,#17722,.F.);
#25415=ORIENTED_EDGE('',*,*,#17723,.T.);
#25416=ORIENTED_EDGE('',*,*,#17719,.T.);
#25417=ORIENTED_EDGE('',*,*,#17724,.T.);
#25418=ORIENTED_EDGE('',*,*,#17725,.F.);
#25419=ORIENTED_EDGE('',*,*,#17726,.T.);
#25420=ORIENTED_EDGE('',*,*,#17722,.T.);
#25421=ORIENTED_EDGE('',*,*,#17727,.T.);
#25422=ORIENTED_EDGE('',*,*,#17728,.F.);
#25423=ORIENTED_EDGE('',*,*,#17729,.F.);
#25424=ORIENTED_EDGE('',*,*,#17730,.T.);
#25425=ORIENTED_EDGE('',*,*,#17725,.T.);
#25426=ORIENTED_EDGE('',*,*,#17731,.T.);
#25427=ORIENTED_EDGE('',*,*,#17732,.F.);
#25428=ORIENTED_EDGE('',*,*,#17733,.T.);
#25429=ORIENTED_EDGE('',*,*,#17734,.F.);
#25430=ORIENTED_EDGE('',*,*,#17735,.F.);
#25431=ORIENTED_EDGE('',*,*,#17736,.F.);
#25432=ORIENTED_EDGE('',*,*,#17737,.T.);
#25433=ORIENTED_EDGE('',*,*,#17732,.T.);
#25434=ORIENTED_EDGE('',*,*,#17738,.F.);
#25435=ORIENTED_EDGE('',*,*,#17739,.F.);
#25436=ORIENTED_EDGE('',*,*,#17740,.T.);
#25437=ORIENTED_EDGE('',*,*,#17736,.T.);
#25438=ORIENTED_EDGE('',*,*,#17741,.F.);
#25439=ORIENTED_EDGE('',*,*,#17742,.F.);
#25440=ORIENTED_EDGE('',*,*,#17743,.T.);
#25441=ORIENTED_EDGE('',*,*,#17739,.T.);
#25442=ORIENTED_EDGE('',*,*,#17744,.F.);
#25443=ORIENTED_EDGE('',*,*,#17745,.F.);
#25444=ORIENTED_EDGE('',*,*,#17746,.T.);
#25445=ORIENTED_EDGE('',*,*,#17742,.T.);
#25446=ORIENTED_EDGE('',*,*,#17747,.F.);
#25447=ORIENTED_EDGE('',*,*,#17748,.F.);
#25448=ORIENTED_EDGE('',*,*,#17749,.T.);
#25449=ORIENTED_EDGE('',*,*,#17745,.T.);
#25450=ORIENTED_EDGE('',*,*,#17750,.F.);
#25451=ORIENTED_EDGE('',*,*,#17751,.F.);
#25452=ORIENTED_EDGE('',*,*,#17752,.T.);
#25453=ORIENTED_EDGE('',*,*,#17748,.T.);
#25454=ORIENTED_EDGE('',*,*,#17753,.F.);
#25455=ORIENTED_EDGE('',*,*,#17754,.F.);
#25456=ORIENTED_EDGE('',*,*,#17755,.T.);
#25457=ORIENTED_EDGE('',*,*,#17751,.T.);
#25458=ORIENTED_EDGE('',*,*,#17756,.F.);
#25459=ORIENTED_EDGE('',*,*,#17757,.F.);
#25460=ORIENTED_EDGE('',*,*,#17758,.T.);
#25461=ORIENTED_EDGE('',*,*,#17754,.T.);
#25462=ORIENTED_EDGE('',*,*,#17759,.F.);
#25463=ORIENTED_EDGE('',*,*,#17760,.F.);
#25464=ORIENTED_EDGE('',*,*,#17761,.T.);
#25465=ORIENTED_EDGE('',*,*,#17757,.T.);
#25466=ORIENTED_EDGE('',*,*,#17762,.F.);
#25467=ORIENTED_EDGE('',*,*,#17763,.F.);
#25468=ORIENTED_EDGE('',*,*,#17764,.T.);
#25469=ORIENTED_EDGE('',*,*,#17760,.T.);
#25470=ORIENTED_EDGE('',*,*,#17765,.F.);
#25471=ORIENTED_EDGE('',*,*,#17766,.F.);
#25472=ORIENTED_EDGE('',*,*,#17767,.T.);
#25473=ORIENTED_EDGE('',*,*,#17763,.T.);
#25474=ORIENTED_EDGE('',*,*,#17768,.F.);
#25475=ORIENTED_EDGE('',*,*,#17769,.F.);
#25476=ORIENTED_EDGE('',*,*,#17770,.F.);
#25477=ORIENTED_EDGE('',*,*,#17731,.F.);
#25478=ORIENTED_EDGE('',*,*,#17727,.F.);
#25479=ORIENTED_EDGE('',*,*,#17724,.F.);
#25480=ORIENTED_EDGE('',*,*,#17721,.F.);
#25481=ORIENTED_EDGE('',*,*,#17718,.F.);
#25482=ORIENTED_EDGE('',*,*,#17715,.F.);
#25483=ORIENTED_EDGE('',*,*,#17712,.F.);
#25484=ORIENTED_EDGE('',*,*,#17709,.F.);
#25485=ORIENTED_EDGE('',*,*,#17706,.F.);
#25486=ORIENTED_EDGE('',*,*,#17703,.F.);
#25487=ORIENTED_EDGE('',*,*,#17700,.F.);
#25488=ORIENTED_EDGE('',*,*,#17697,.F.);
#25489=ORIENTED_EDGE('',*,*,#17694,.F.);
#25490=ORIENTED_EDGE('',*,*,#17771,.F.);
#25491=ORIENTED_EDGE('',*,*,#17772,.T.);
#25492=ORIENTED_EDGE('',*,*,#17768,.T.);
#25493=ORIENTED_EDGE('',*,*,#17765,.T.);
#25494=ORIENTED_EDGE('',*,*,#17762,.T.);
#25495=ORIENTED_EDGE('',*,*,#17759,.T.);
#25496=ORIENTED_EDGE('',*,*,#17756,.T.);
#25497=ORIENTED_EDGE('',*,*,#17753,.T.);
#25498=ORIENTED_EDGE('',*,*,#17750,.T.);
#25499=ORIENTED_EDGE('',*,*,#17747,.T.);
#25500=ORIENTED_EDGE('',*,*,#17744,.T.);
#25501=ORIENTED_EDGE('',*,*,#17741,.T.);
#25502=ORIENTED_EDGE('',*,*,#17738,.T.);
#25503=ORIENTED_EDGE('',*,*,#17735,.T.);
#25504=ORIENTED_EDGE('',*,*,#17773,.T.);
#25505=ORIENTED_EDGE('',*,*,#17774,.T.);
#25506=ORIENTED_EDGE('',*,*,#17775,.T.);
#25507=ORIENTED_EDGE('',*,*,#17776,.T.);
#25508=ORIENTED_EDGE('',*,*,#17771,.T.);
#25509=ORIENTED_EDGE('',*,*,#17766,.T.);
#25510=ORIENTED_EDGE('',*,*,#17772,.F.);
#25511=ORIENTED_EDGE('',*,*,#17776,.F.);
#25512=ORIENTED_EDGE('',*,*,#17777,.T.);
#25513=ORIENTED_EDGE('',*,*,#17778,.F.);
#25514=ORIENTED_EDGE('',*,*,#17733,.F.);
#25515=ORIENTED_EDGE('',*,*,#17737,.F.);
#25516=ORIENTED_EDGE('',*,*,#17740,.F.);
#25517=ORIENTED_EDGE('',*,*,#17743,.F.);
#25518=ORIENTED_EDGE('',*,*,#17746,.F.);
#25519=ORIENTED_EDGE('',*,*,#17749,.F.);
#25520=ORIENTED_EDGE('',*,*,#17752,.F.);
#25521=ORIENTED_EDGE('',*,*,#17755,.F.);
#25522=ORIENTED_EDGE('',*,*,#17758,.F.);
#25523=ORIENTED_EDGE('',*,*,#17761,.F.);
#25524=ORIENTED_EDGE('',*,*,#17764,.F.);
#25525=ORIENTED_EDGE('',*,*,#17767,.F.);
#25526=ORIENTED_EDGE('',*,*,#17777,.F.);
#25527=ORIENTED_EDGE('',*,*,#17775,.F.);
#25528=ORIENTED_EDGE('',*,*,#17692,.F.);
#25529=ORIENTED_EDGE('',*,*,#17696,.F.);
#25530=ORIENTED_EDGE('',*,*,#17699,.F.);
#25531=ORIENTED_EDGE('',*,*,#17702,.F.);
#25532=ORIENTED_EDGE('',*,*,#17705,.F.);
#25533=ORIENTED_EDGE('',*,*,#17708,.F.);
#25534=ORIENTED_EDGE('',*,*,#17711,.F.);
#25535=ORIENTED_EDGE('',*,*,#17714,.F.);
#25536=ORIENTED_EDGE('',*,*,#17717,.F.);
#25537=ORIENTED_EDGE('',*,*,#17720,.F.);
#25538=ORIENTED_EDGE('',*,*,#17723,.F.);
#25539=ORIENTED_EDGE('',*,*,#17726,.F.);
#25540=ORIENTED_EDGE('',*,*,#17730,.F.);
#25541=ORIENTED_EDGE('',*,*,#17779,.F.);
#25542=ORIENTED_EDGE('',*,*,#17780,.T.);
#25543=ORIENTED_EDGE('',*,*,#17781,.T.);
#25544=ORIENTED_EDGE('',*,*,#17782,.F.);
#25545=ORIENTED_EDGE('',*,*,#17783,.F.);
#25546=ORIENTED_EDGE('',*,*,#17782,.T.);
#25547=ORIENTED_EDGE('',*,*,#17784,.T.);
#25548=ORIENTED_EDGE('',*,*,#17785,.F.);
#25549=ORIENTED_EDGE('',*,*,#17786,.F.);
#25550=ORIENTED_EDGE('',*,*,#17785,.T.);
#25551=ORIENTED_EDGE('',*,*,#17787,.T.);
#25552=ORIENTED_EDGE('',*,*,#17788,.F.);
#25553=ORIENTED_EDGE('',*,*,#17789,.F.);
#25554=ORIENTED_EDGE('',*,*,#17788,.T.);
#25555=ORIENTED_EDGE('',*,*,#17790,.T.);
#25556=ORIENTED_EDGE('',*,*,#17791,.F.);
#25557=ORIENTED_EDGE('',*,*,#17792,.F.);
#25558=ORIENTED_EDGE('',*,*,#17793,.T.);
#25559=ORIENTED_EDGE('',*,*,#17794,.T.);
#25560=ORIENTED_EDGE('',*,*,#17780,.F.);
#25561=ORIENTED_EDGE('',*,*,#17795,.F.);
#25562=ORIENTED_EDGE('',*,*,#17791,.T.);
#25563=ORIENTED_EDGE('',*,*,#17796,.T.);
#25564=ORIENTED_EDGE('',*,*,#17793,.F.);
#25565=ORIENTED_EDGE('',*,*,#17796,.F.);
#25566=ORIENTED_EDGE('',*,*,#17790,.F.);
#25567=ORIENTED_EDGE('',*,*,#17787,.F.);
#25568=ORIENTED_EDGE('',*,*,#17784,.F.);
#25569=ORIENTED_EDGE('',*,*,#17781,.F.);
#25570=ORIENTED_EDGE('',*,*,#17794,.F.);
#25571=ORIENTED_EDGE('',*,*,#17797,.F.);
#25572=ORIENTED_EDGE('',*,*,#17773,.F.);
#25573=ORIENTED_EDGE('',*,*,#17693,.F.);
#25574=ORIENTED_EDGE('',*,*,#17774,.F.);
#25575=ORIENTED_EDGE('',*,*,#17798,.T.);
#25576=ORIENTED_EDGE('',*,*,#17797,.T.);
#25577=ORIENTED_EDGE('',*,*,#17798,.F.);
#25578=ORIENTED_EDGE('',*,*,#17728,.T.);
#25579=ORIENTED_EDGE('',*,*,#17770,.T.);
#25580=ORIENTED_EDGE('',*,*,#17799,.F.);
#25581=ORIENTED_EDGE('',*,*,#17800,.F.);
#25582=ORIENTED_EDGE('',*,*,#17729,.T.);
#25583=ORIENTED_EDGE('',*,*,#17799,.T.);
#25584=ORIENTED_EDGE('',*,*,#17769,.T.);
#25585=ORIENTED_EDGE('',*,*,#17734,.T.);
#25586=ORIENTED_EDGE('',*,*,#17778,.T.);
#25587=ORIENTED_EDGE('',*,*,#17789,.T.);
#25588=ORIENTED_EDGE('',*,*,#17795,.T.);
#25589=ORIENTED_EDGE('',*,*,#17792,.T.);
#25590=ORIENTED_EDGE('',*,*,#17779,.T.);
#25591=ORIENTED_EDGE('',*,*,#17783,.T.);
#25592=ORIENTED_EDGE('',*,*,#17786,.T.);
#25593=ORIENTED_EDGE('',*,*,#17801,.T.);
#25594=ORIENTED_EDGE('',*,*,#17800,.T.);
#25595=ORIENTED_EDGE('',*,*,#17801,.F.);
#27180=ADVANCED_FACE('',(#8356),#6800,.T.);
#27181=ADVANCED_FACE('',(#8357),#6801,.T.);
#27182=ADVANCED_FACE('',(#8358),#6802,.T.);
#27183=ADVANCED_FACE('',(#8359),#6803,.T.);
#27184=ADVANCED_FACE('',(#8360),#6804,.T.);
#27185=ADVANCED_FACE('',(#8361),#6805,.T.);
#27186=ADVANCED_FACE('',(#8362),#6806,.T.);
#27187=ADVANCED_FACE('',(#8363),#6807,.T.);
#27188=ADVANCED_FACE('',(#8364),#6808,.T.);
#27189=ADVANCED_FACE('',(#8365),#6809,.T.);
#27190=ADVANCED_FACE('',(#8366),#6810,.T.);
#27191=ADVANCED_FACE('',(#8367),#6811,.T.);
#27192=ADVANCED_FACE('',(#8368),#6812,.T.);
#27193=ADVANCED_FACE('',(#8369),#6813,.T.);
#27194=ADVANCED_FACE('',(#8370),#6814,.T.);
#27195=ADVANCED_FACE('',(#8371),#6815,.T.);
#27196=ADVANCED_FACE('',(#8372),#6816,.T.);
#27197=ADVANCED_FACE('',(#8373),#6817,.T.);
#27198=ADVANCED_FACE('',(#8374),#6818,.T.);
#27199=ADVANCED_FACE('',(#8375),#6819,.T.);
#27200=ADVANCED_FACE('',(#8376),#6820,.T.);
#27201=ADVANCED_FACE('',(#8377),#6821,.T.);
#27202=ADVANCED_FACE('',(#8378),#6822,.T.);
#27203=ADVANCED_FACE('',(#8379),#6823,.T.);
#27204=ADVANCED_FACE('',(#8380),#6824,.T.);
#27205=ADVANCED_FACE('',(#8381),#582,.F.);
#27206=ADVANCED_FACE('',(#8382),#1748,.T.);
#27207=ADVANCED_FACE('',(#8383),#6825,.T.);
#27208=ADVANCED_FACE('',(#8384),#583,.F.);
#27209=ADVANCED_FACE('',(#8385),#1749,.F.);
#27210=ADVANCED_FACE('',(#8386),#1750,.F.);
#27211=ADVANCED_FACE('',(#8387),#1751,.F.);
#27212=ADVANCED_FACE('',(#8388),#1752,.F.);
#27213=ADVANCED_FACE('',(#8389),#1753,.F.);
#27214=ADVANCED_FACE('',(#8390),#1754,.F.);
#27215=ADVANCED_FACE('',(#8391),#1755,.F.);
#27216=ADVANCED_FACE('',(#8392),#1756,.T.);
#27217=ADVANCED_FACE('',(#8393),#411,.T.);
#27218=ADVANCED_FACE('',(#8394),#6826,.T.);
#27219=ADVANCED_FACE('',(#8395,#756),#1757,.T.);
#27220=ADVANCED_FACE('',(#8396),#604,.F.);
#27240=CLOSED_SHELL('',(#27180,#27181,#27182,#27183,#27184,#27185,#27186,
#27187,#27188,#27189,#27190,#27191,#27192,#27193,#27194,#27195,#27196,#27197,
#27198,#27199,#27200,#27201,#27202,#27203,#27204,#27205,#27206,#27207,#27208,
#27209,#27210,#27211,#27212,#27213,#27214,#27215,#27216,#27217,#27218,#27219,
#27220));
#29892=AXIS2_PLACEMENT_3D('',#53617,#37169,#37170);
#29893=AXIS2_PLACEMENT_3D('',#53618,#37171,#37172);
#29894=AXIS2_PLACEMENT_3D('',#53634,#37174,#37175);
#29895=AXIS2_PLACEMENT_3D('',#53642,#37176,#37177);
#29896=AXIS2_PLACEMENT_3D('',#53690,#37179,#37180);
#29897=AXIS2_PLACEMENT_3D('',#53738,#37182,#37183);
#29898=AXIS2_PLACEMENT_3D('',#53792,#37185,#37186);
#29899=AXIS2_PLACEMENT_3D('',#53840,#37188,#37189);
#29900=AXIS2_PLACEMENT_3D('',#53888,#37191,#37192);
#29901=AXIS2_PLACEMENT_3D('',#53936,#37194,#37195);
#29902=AXIS2_PLACEMENT_3D('',#53990,#37197,#37198);
#29903=AXIS2_PLACEMENT_3D('',#54038,#37200,#37201);
#29904=AXIS2_PLACEMENT_3D('',#54086,#37203,#37204);
#29905=AXIS2_PLACEMENT_3D('',#54140,#37206,#37207);
#29906=AXIS2_PLACEMENT_3D('',#54188,#37209,#37210);
#29907=AXIS2_PLACEMENT_3D('',#54193,#37212,#37213);
#29908=AXIS2_PLACEMENT_3D('',#54235,#37214,#37215);
#29909=AXIS2_PLACEMENT_3D('',#54248,#37217,#37218);
#29910=AXIS2_PLACEMENT_3D('',#54255,#37219,#37220);
#29911=AXIS2_PLACEMENT_3D('',#54279,#37222,#37223);
#29912=AXIS2_PLACEMENT_3D('',#54304,#37225,#37226);
#29913=AXIS2_PLACEMENT_3D('',#54329,#37228,#37229);
#29914=AXIS2_PLACEMENT_3D('',#54353,#37231,#37232);
#29915=AXIS2_PLACEMENT_3D('',#54378,#37234,#37235);
#29916=AXIS2_PLACEMENT_3D('',#54403,#37237,#37238);
#29917=AXIS2_PLACEMENT_3D('',#54427,#37240,#37241);
#29918=AXIS2_PLACEMENT_3D('',#54451,#37243,#37244);
#29919=AXIS2_PLACEMENT_3D('',#54476,#37246,#37247);
#29920=AXIS2_PLACEMENT_3D('',#54501,#37249,#37250);
#29921=AXIS2_PLACEMENT_3D('',#55038,#37252,#37253);
#29922=AXIS2_PLACEMENT_3D('',#55040,#37254,#37255);
#29923=AXIS2_PLACEMENT_3D('',#55041,#37256,#37257);
#29924=AXIS2_PLACEMENT_3D('',#55128,#37258,#37259);
#29925=AXIS2_PLACEMENT_3D('',#55129,#37260,#37261);
#29926=AXIS2_PLACEMENT_3D('',#55551,#37262,#37263);
#29927=AXIS2_PLACEMENT_3D('',#55565,#37267,#37268);
#29928=AXIS2_PLACEMENT_3D('',#55576,#37271,#37272);
#29929=AXIS2_PLACEMENT_3D('',#55587,#37275,#37276);
#29930=AXIS2_PLACEMENT_3D('',#55598,#37279,#37280);
#29931=AXIS2_PLACEMENT_3D('',#55609,#37283,#37284);
#29932=AXIS2_PLACEMENT_3D('',#55617,#37286,#37287);
#29933=AXIS2_PLACEMENT_3D('',#55618,#37288,#37289);
#29934=AXIS2_PLACEMENT_3D('',#55620,#37290,#37291);
#29935=AXIS2_PLACEMENT_3D('',#55621,#37292,#37293);
#29936=AXIS2_PLACEMENT_3D('',#55623,#37295,#37296);
#29937=AXIS2_PLACEMENT_3D('',#55624,#37297,#37298);
#29938=AXIS2_PLACEMENT_3D('',#55625,#37299,#37300);
#29939=AXIS2_PLACEMENT_3D('',#55627,#37301,#37302);
#37169=DIRECTION('axis',(0.,0.,1.));
#37170=DIRECTION('refdir',(1.,0.,0.));
#37171=DIRECTION('center_axis',(1.,0.,0.));
#37172=DIRECTION('ref_axis',(0.,1.,0.));
#37173=DIRECTION('',(-1.,0.,0.));
#37174=DIRECTION('center_axis',(1.,0.,0.));
#37175=DIRECTION('ref_axis',(0.,1.,0.));
#37176=DIRECTION('center_axis',(1.,0.,0.));
#37177=DIRECTION('ref_axis',(0.,1.,0.));
#37178=DIRECTION('',(-1.,0.,0.));
#37179=DIRECTION('center_axis',(1.,0.,0.));
#37180=DIRECTION('ref_axis',(0.,1.,0.));
#37181=DIRECTION('',(-1.,0.,0.));
#37182=DIRECTION('center_axis',(1.,0.,0.));
#37183=DIRECTION('ref_axis',(0.,1.,0.));
#37184=DIRECTION('',(-1.,0.,0.));
#37185=DIRECTION('center_axis',(1.,0.,0.));
#37186=DIRECTION('ref_axis',(0.,1.,0.));
#37187=DIRECTION('',(-1.,0.,0.));
#37188=DIRECTION('center_axis',(1.,0.,0.));
#37189=DIRECTION('ref_axis',(0.,1.,0.));
#37190=DIRECTION('',(-1.,0.,0.));
#37191=DIRECTION('center_axis',(1.,0.,0.));
#37192=DIRECTION('ref_axis',(0.,1.,0.));
#37193=DIRECTION('',(-1.,0.,0.));
#37194=DIRECTION('center_axis',(1.,0.,0.));
#37195=DIRECTION('ref_axis',(0.,1.,0.));
#37196=DIRECTION('',(-1.,0.,0.));
#37197=DIRECTION('center_axis',(1.,0.,0.));
#37198=DIRECTION('ref_axis',(0.,1.,0.));
#37199=DIRECTION('',(-1.,0.,0.));
#37200=DIRECTION('center_axis',(1.,0.,0.));
#37201=DIRECTION('ref_axis',(0.,1.,0.));
#37202=DIRECTION('',(-1.,0.,0.));
#37203=DIRECTION('center_axis',(1.,0.,0.));
#37204=DIRECTION('ref_axis',(0.,1.,0.));
#37205=DIRECTION('',(-1.,0.,0.));
#37206=DIRECTION('center_axis',(1.,0.,0.));
#37207=DIRECTION('ref_axis',(0.,1.,0.));
#37208=DIRECTION('',(-1.,0.,0.));
#37209=DIRECTION('center_axis',(1.,0.,0.));
#37210=DIRECTION('ref_axis',(0.,1.,0.));
#37211=DIRECTION('',(-1.,0.,0.));
#37212=DIRECTION('center_axis',(1.,0.,0.));
#37213=DIRECTION('ref_axis',(0.,1.,0.));
#37214=DIRECTION('center_axis',(1.,0.,0.));
#37215=DIRECTION('ref_axis',(0.,1.,6.79493845743686E-14));
#37216=DIRECTION('',(1.,0.,0.));
#37217=DIRECTION('center_axis',(1.,0.,0.));
#37218=DIRECTION('ref_axis',(0.,1.,6.79493845743686E-14));
#37219=DIRECTION('center_axis',(1.,0.,0.));
#37220=DIRECTION('ref_axis',(0.,1.,6.79493845743686E-14));
#37221=DIRECTION('',(1.,0.,0.));
#37222=DIRECTION('center_axis',(1.,0.,0.));
#37223=DIRECTION('ref_axis',(0.,1.,6.79493845743686E-14));
#37224=DIRECTION('',(1.,0.,0.));
#37225=DIRECTION('center_axis',(1.,0.,0.));
#37226=DIRECTION('ref_axis',(0.,1.,6.79493845743686E-14));
#37227=DIRECTION('',(1.,0.,0.));
#37228=DIRECTION('center_axis',(1.,0.,0.));
#37229=DIRECTION('ref_axis',(0.,1.,6.79493845743686E-14));
#37230=DIRECTION('',(1.,0.,0.));
#37231=DIRECTION('center_axis',(1.,0.,0.));
#37232=DIRECTION('ref_axis',(0.,1.,6.79493845743686E-14));
#37233=DIRECTION('',(1.,0.,0.));
#37234=DIRECTION('center_axis',(1.,0.,0.));
#37235=DIRECTION('ref_axis',(0.,1.,6.79493845743686E-14));
#37236=DIRECTION('',(1.,0.,0.));
#37237=DIRECTION('center_axis',(1.,0.,0.));
#37238=DIRECTION('ref_axis',(0.,1.,6.79493845743686E-14));
#37239=DIRECTION('',(1.,0.,0.));
#37240=DIRECTION('center_axis',(1.,0.,0.));
#37241=DIRECTION('ref_axis',(0.,1.,6.79493845743686E-14));
#37242=DIRECTION('',(1.,0.,0.));
#37243=DIRECTION('center_axis',(1.,0.,0.));
#37244=DIRECTION('ref_axis',(0.,1.,6.79493845743686E-14));
#37245=DIRECTION('',(1.,0.,0.));
#37246=DIRECTION('center_axis',(1.,0.,0.));
#37247=DIRECTION('ref_axis',(0.,1.,6.79493845743686E-14));
#37248=DIRECTION('',(1.,0.,0.));
#37249=DIRECTION('center_axis',(1.,0.,0.));
#37250=DIRECTION('ref_axis',(0.,1.,6.79493845743686E-14));
#37251=DIRECTION('',(1.,0.,0.));
#37252=DIRECTION('center_axis',(1.,0.,0.));
#37253=DIRECTION('ref_axis',(0.,0.,-1.));
#37254=DIRECTION('center_axis',(1.,0.,0.));
#37255=DIRECTION('ref_axis',(0.,1.,0.));
#37256=DIRECTION('center_axis',(1.,0.,0.));
#37257=DIRECTION('ref_axis',(0.,1.,0.));
#37258=DIRECTION('center_axis',(-1.,0.,0.));
#37259=DIRECTION('ref_axis',(0.,1.,6.79493845743686E-14));
#37260=DIRECTION('center_axis',(1.,0.,0.));
#37261=DIRECTION('ref_axis',(0.,1.,6.79493845743686E-14));
#37262=DIRECTION('center_axis',(0.,-0.5,-0.866025403784439));
#37263=DIRECTION('ref_axis',(0.,-0.866025403784439,0.5));
#37264=DIRECTION('',(-1.,0.,0.));
#37265=DIRECTION('',(0.,-0.866025403784439,0.5));
#37266=DIRECTION('',(-1.,0.,0.));
#37267=DIRECTION('center_axis',(0.,-1.,-1.60246890531964E-16));
#37268=DIRECTION('ref_axis',(0.,-1.60246890531964E-16,1.));
#37269=DIRECTION('',(0.,-1.60246890531964E-16,1.));
#37270=DIRECTION('',(-1.,0.,0.));
#37271=DIRECTION('center_axis',(0.,-0.5,0.866025403784439));
#37272=DIRECTION('ref_axis',(0.,0.866025403784439,0.5));
#37273=DIRECTION('',(0.,0.866025403784439,0.5));
#37274=DIRECTION('',(-1.,0.,0.));
#37275=DIRECTION('center_axis',(0.,0.5,0.866025403784439));
#37276=DIRECTION('ref_axis',(0.,0.866025403784439,-0.5));
#37277=DIRECTION('',(0.,0.866025403784439,-0.5));
#37278=DIRECTION('',(-1.,0.,0.));
#37279=DIRECTION('center_axis',(0.,0.5,-0.866025403784439));
#37280=DIRECTION('ref_axis',(0.,-0.866025403784439,-0.5));
#37281=DIRECTION('',(-1.,0.,0.));
#37282=DIRECTION('',(0.,-0.866025403784439,-0.5));
#37283=DIRECTION('center_axis',(0.,1.,-3.20493781063927E-16));
#37284=DIRECTION('ref_axis',(0.,-3.20493781063927E-16,-1.));
#37285=DIRECTION('',(0.,-3.20493781063927E-16,-1.));
#37286=DIRECTION('center_axis',(-1.,0.,0.));
#37287=DIRECTION('ref_axis',(0.,0.,1.));
#37288=DIRECTION('center_axis',(-1.,0.,0.));
#37289=DIRECTION('ref_axis',(0.,0.,1.));
#37290=DIRECTION('center_axis',(1.,0.,0.));
#37291=DIRECTION('ref_axis',(0.,0.,-1.));
#37292=DIRECTION('center_axis',(1.,0.,0.));
#37293=DIRECTION('ref_axis',(0.,1.,0.));
#37294=DIRECTION('',(-0.707106781186548,0.707106781186547,8.65956056235493E-17));
#37295=DIRECTION('center_axis',(1.,0.,0.));
#37296=DIRECTION('ref_axis',(0.,1.,0.));
#37297=DIRECTION('center_axis',(1.,0.,0.));
#37298=DIRECTION('ref_axis',(0.,1.,0.));
#37299=DIRECTION('center_axis',(-1.,0.,0.));
#37300=DIRECTION('ref_axis',(0.,0.,1.));
#37301=DIRECTION('center_axis',(1.,0.,0.));
#37302=DIRECTION('ref_axis',(0.,0.,-1.));
#53617=CARTESIAN_POINT('',(0.,0.,0.));
#53618=CARTESIAN_POINT('Origin',(-4.85,0.,0.));
#53619=CARTESIAN_POINT('',(-9.49167250378795,-2.45327747456172,0.00165524322402417));
#53620=CARTESIAN_POINT('',(-9.60732749621206,-2.45271517060122,0.00261677541903093));
#53621=CARTESIAN_POINT('',(-4.85,-2.4505,-3.00099698131059E-16));
#53622=CARTESIAN_POINT('',(-9.7495,1.07637022042037,2.20364147798228));
#53623=CARTESIAN_POINT('Ctrl Pts',(-9.49167250378795,-2.45327747456172,
0.00165524322402417));
#53624=CARTESIAN_POINT('Ctrl Pts',(-9.49633463918664,-2.4539194957778,0.0910866010723908));
#53625=CARTESIAN_POINT('Ctrl Pts',(-9.50099677458534,-2.44945222484254,
0.180449214552893));
#53626=CARTESIAN_POINT('Ctrl Pts',(-9.50565890998403,-2.43966236895119,
0.269219861232167));
#53627=CARTESIAN_POINT('Ctrl Pts',(-9.54790628291729,-2.3509485806471,1.07364236188226));
#53628=CARTESIAN_POINT('Ctrl Pts',(-9.59015365585055,-1.825163527862,1.82945470779013));
#53629=CARTESIAN_POINT('Ctrl Pts',(-9.63240102878381,-1.10182743978963,
2.19303587121579));
#53630=CARTESIAN_POINT('Ctrl Pts',(-9.67143401918921,-0.433526226594529,
2.52895403791445));
#53631=CARTESIAN_POINT('Ctrl Pts',(-9.7104670095946,0.4034083658124,2.53005609171326));
#53632=CARTESIAN_POINT('Ctrl Pts',(-9.7495,1.07765198048948,2.20520778639847));
#53633=CARTESIAN_POINT('',(-9.7495,-1.07508846035133,2.20207516956606));
#53634=CARTESIAN_POINT('Origin',(-9.7495,0.,0.));
#53635=CARTESIAN_POINT('Ctrl Pts',(-9.7495,-1.07508846035133,2.20207516956606));
#53636=CARTESIAN_POINT('Ctrl Pts',(-9.70725262706674,-1.80575922297742,
1.8453499695947));
#53637=CARTESIAN_POINT('Ctrl Pts',(-9.66500525413347,-2.33873961907574,
1.09958288884865));
#53638=CARTESIAN_POINT('Ctrl Pts',(-9.62275788120021,-2.43620643494331,
0.297400442061077));
#53639=CARTESIAN_POINT('Ctrl Pts',(-9.61761441953749,-2.448072659894,0.199737691099642));
#53640=CARTESIAN_POINT('Ctrl Pts',(-9.61247095787478,-2.45348363138364,
0.101238742362921));
#53641=CARTESIAN_POINT('Ctrl Pts',(-9.60732749621206,-2.45271517060122,
0.00261677541903093));
#53642=CARTESIAN_POINT('Origin',(-4.85,0.,0.));
#53643=CARTESIAN_POINT('',(-8.69167250378794,-2.44691142445882,0.000997465547478843));
#53644=CARTESIAN_POINT('',(-8.80732749621206,-2.44679980543952,0.000874454649755137));
#53645=CARTESIAN_POINT('',(-4.85,-2.4505,-3.00099698131059E-16));
#53646=CARTESIAN_POINT('Ctrl Pts',(-8.69167250378794,-2.44691142445882,
0.000997465547478843));
#53647=CARTESIAN_POINT('Ctrl Pts',(-8.70951706825373,-2.4481762977678,0.345611269438561));
#53648=CARTESIAN_POINT('Ctrl Pts',(-8.72736163271951,-2.38025527099653,
0.689748316659788));
#53649=CARTESIAN_POINT('Ctrl Pts',(-8.7452061971853,-2.24070602085676,1.00185768813625));
#53650=CARTESIAN_POINT('Ctrl Pts',(-8.78745357011856,-1.91032030454994,
1.74078303641323));
#53651=CARTESIAN_POINT('Ctrl Pts',(-8.82970094305183,-1.17844740017566,
2.30018834537626));
#53652=CARTESIAN_POINT('Ctrl Pts',(-8.8719483159851,-0.378714078450958,
2.42508315806902));
#53653=CARTESIAN_POINT('Ctrl Pts',(-8.91419568891836,0.42101924327374,2.54997797076177));
#53654=CARTESIAN_POINT('Ctrl Pts',(-8.95644306185162,1.28861298234885,2.24036228718424));
#53655=CARTESIAN_POINT('Ctrl Pts',(-8.99869043478488,1.82856107840019,1.63734074473426));
#53656=CARTESIAN_POINT('Ctrl Pts',(-9.04093780771814,2.36850917445153,1.03431920228428));
#53657=CARTESIAN_POINT('Ctrl Pts',(-9.0831851806514,2.5808116274791,0.137891800961835));
#53658=CARTESIAN_POINT('Ctrl Pts',(-9.12543255358466,2.36870098520686,-0.643228817589892));
#53659=CARTESIAN_POINT('Ctrl Pts',(-9.16767992651792,2.15659034293461,-1.42434943614162));
#53660=CARTESIAN_POINT('Ctrl Pts',(-9.20992729945119,1.52006660536256,-2.09016327192263));
#53661=CARTESIAN_POINT('Ctrl Pts',(-9.25217467238445,0.749270724461215,
-2.33728533022963));
#53662=CARTESIAN_POINT('Ctrl Pts',(-9.29442204531772,-0.0215251564401345,
-2.58440738853662));
#53663=CARTESIAN_POINT('Ctrl Pts',(-9.33666941825097,-0.926593180670786,
-2.4128376693696));
#53664=CARTESIAN_POINT('Ctrl Pts',(-9.37891679118423,-1.55330593087457,
-1.90053648208992));
#53665=CARTESIAN_POINT('Ctrl Pts',(-9.4165020287188,-2.11085888498516,-1.44476940176601));
#53666=CARTESIAN_POINT('Ctrl Pts',(-9.45408726625338,-2.44810162318784,
-0.719323136921701));
#53667=CARTESIAN_POINT('Ctrl Pts',(-9.49167250378795,-2.45327747456172,
0.00165524322402417));
#53668=CARTESIAN_POINT('Ctrl Pts',(-9.60732749621206,-2.45271517060122,
0.00261677541903093));
#53669=CARTESIAN_POINT('Ctrl Pts',(-9.57022358494152,-2.44717164708428,
-0.708822514065269));
#53670=CARTESIAN_POINT('Ctrl Pts',(-9.53311967367097,-2.12005707050393,
-1.42666353961262));
#53671=CARTESIAN_POINT('Ctrl Pts',(-9.49601576240043,-1.57491430716428,
-1.88317974641052));
#53672=CARTESIAN_POINT('Ctrl Pts',(-9.45376838946716,-0.954202127880854,
-2.40297967526545));
#53673=CARTESIAN_POINT('Ctrl Pts',(-9.4115210165339,-0.0508245336771831,
-2.5839817201462));
#53674=CARTESIAN_POINT('Ctrl Pts',(-9.36927364360064,0.7227993233438,-2.34541864510377));
#53675=CARTESIAN_POINT('Ctrl Pts',(-9.32702627066737,1.49642318036478,-2.10685557006134));
#53676=CARTESIAN_POINT('Ctrl Pts',(-9.28477889773412,2.14029330020308,-1.44872737509573));
#53677=CARTESIAN_POINT('Ctrl Pts',(-9.24253152480085,2.36120984472134,-0.670163752243124));
#53678=CARTESIAN_POINT('Ctrl Pts',(-9.20028415186759,2.58212638923961,0.108399870609487));
#53679=CARTESIAN_POINT('Ctrl Pts',(-9.15803677893433,2.38008935843785,1.0073989213491));
#53680=CARTESIAN_POINT('Ctrl Pts',(-9.11578940600107,1.84703509648051,1.61655781423769));
#53681=CARTESIAN_POINT('Ctrl Pts',(-9.0735420330678,1.31398083452317,2.22571670712627));
#53682=CARTESIAN_POINT('Ctrl Pts',(-9.03129466013454,0.449909341410258,
2.54503544216384));
#53683=CARTESIAN_POINT('Ctrl Pts',(-8.98904728720128,-0.351199568854151,
2.42919060595784));
#53684=CARTESIAN_POINT('Ctrl Pts',(-8.94679991426801,-1.15230847911856,
2.31334576975184));
#53685=CARTESIAN_POINT('Ctrl Pts',(-8.90455254133475,-1.89045480653447,
1.76233736230228));
#53686=CARTESIAN_POINT('Ctrl Pts',(-8.86230516840149,-2.22919361727906,
1.02722088666372));
#53687=CARTESIAN_POINT('Ctrl Pts',(-8.84397927767168,-2.37613033785236,
0.708345101712173));
#53688=CARTESIAN_POINT('Ctrl Pts',(-8.82565338694187,-2.44791394062357,
0.354827266324934));
#53689=CARTESIAN_POINT('Ctrl Pts',(-8.80732749621206,-2.44679980543952,
0.000874454649755137));
#53690=CARTESIAN_POINT('Origin',(-4.85,0.,0.));
#53691=CARTESIAN_POINT('',(-7.89167250378795,-2.44971218776673,-0.00219053278463388));
#53692=CARTESIAN_POINT('',(-8.00732749621207,-2.44998306124988,-0.00220861612412772));
#53693=CARTESIAN_POINT('',(-4.85,-2.4505,-3.00099698131059E-16));
#53694=CARTESIAN_POINT('Ctrl Pts',(-7.89167250378795,-2.44971218776673,
-0.00219053278463388));
#53695=CARTESIAN_POINT('Ctrl Pts',(-7.92269949732083,-2.44447247776505,
0.595274393060675));
#53696=CARTESIAN_POINT('Ctrl Pts',(-7.95372649085371,-2.22417636360755,
1.19619884911934));
#53697=CARTESIAN_POINT('Ctrl Pts',(-7.98475348438658,-1.82728666671986,
1.63875025584126));
#53698=CARTESIAN_POINT('Ctrl Pts',(-8.02700085731984,-1.28686862653767,
2.24134277909389));
#53699=CARTESIAN_POINT('Ctrl Pts',(-8.0692482302531,-0.419038321458612,
2.55030470728015));
#53700=CARTESIAN_POINT('Ctrl Pts',(-8.11149560318637,0.380596882636705,
2.42479364987812));
#53701=CARTESIAN_POINT('Ctrl Pts',(-8.15374297611963,1.18023208673203,2.29928259247609));
#53702=CARTESIAN_POINT('Ctrl Pts',(-8.19599034905289,1.9116721898436,1.73929854948577));
#53703=CARTESIAN_POINT('Ctrl Pts',(-8.23823772198616,2.24148419393013,1.00011400763455));
#53704=CARTESIAN_POINT('Ctrl Pts',(-8.28048509491942,2.57129619801665,0.260929465783332));
#53705=CARTESIAN_POINT('Ctrl Pts',(-8.32273246785268,2.49948010307813,-0.657455574928778));
#53706=CARTESIAN_POINT('Ctrl Pts',(-8.36497984078594,2.05877411056465,-1.33638646263042));
#53707=CARTESIAN_POINT('Ctrl Pts',(-8.40722721371921,1.61806811805117,-2.01531735033206));
#53708=CARTESIAN_POINT('Ctrl Pts',(-8.44947458665247,0.808472227962739,
-2.45479408502322));
#53709=CARTESIAN_POINT('Ctrl Pts',(-8.49172195958573,-0.0009532390009169,
-2.4544803883035));
#53710=CARTESIAN_POINT('Ctrl Pts',(-8.53396933251899,-0.810378705964571,
-2.45416669158379));
#53711=CARTESIAN_POINT('Ctrl Pts',(-8.57621670545226,-1.61963374980345,
-2.01406256345319));
#53712=CARTESIAN_POINT('Ctrl Pts',(-8.61846407838552,-2.0598120076032,-1.33478780559243));
#53713=CARTESIAN_POINT('Ctrl Pts',(-8.64286688685299,-2.3140665321059,-0.942427034685969));
#53714=CARTESIAN_POINT('Ctrl Pts',(-8.66726969532047,-2.44518168422594,
-0.47026899028148));
#53715=CARTESIAN_POINT('Ctrl Pts',(-8.69167250378794,-2.44691142445882,
0.000997465547478843));
#53716=CARTESIAN_POINT('Ctrl Pts',(-8.80732749621206,-2.44679980543952,
0.000874454649755137));
#53717=CARTESIAN_POINT('Ctrl Pts',(-8.78340601400861,-2.44534548240713,
-0.461153613190768));
#53718=CARTESIAN_POINT('Ctrl Pts',(-8.75948453180516,-2.31968016518885,
-0.923922840341414));
#53719=CARTESIAN_POINT('Ctrl Pts',(-8.73556304960171,-2.07482021352832,
-1.311350703522));
#53720=CARTESIAN_POINT('Ctrl Pts',(-8.69331567666844,-1.64237670495972,
-1.99558127424157));
#53721=CARTESIAN_POINT('Ctrl Pts',(-8.65106830373517,-0.83815839374923,
-2.44481787185314));
#53722=CARTESIAN_POINT('Ctrl Pts',(-8.60882093080191,-0.0287870535078842,
-2.45430704848734));
#53723=CARTESIAN_POINT('Ctrl Pts',(-8.56657355786865,0.780584286733466,
-2.46379622512154));
#53724=CARTESIAN_POINT('Ctrl Pts',(-8.5243261849354,1.59510865600568,-2.03353798077836));
#53725=CARTESIAN_POINT('Ctrl Pts',(-8.48207881200214,2.04348504860573,-1.35965082042215));
#53726=CARTESIAN_POINT('Ctrl Pts',(-8.43983143906888,2.49186144120578,-0.685763660065949));
#53727=CARTESIAN_POINT('Ctrl Pts',(-8.39758406613561,2.57408985713368,0.23175241630329));
#53728=CARTESIAN_POINT('Ctrl Pts',(-8.35533669320234,2.25268240724564,0.974630779216524));
#53729=CARTESIAN_POINT('Ctrl Pts',(-8.31308932026908,1.93127495735761,1.71750914212977));
#53730=CARTESIAN_POINT('Ctrl Pts',(-8.27084194733582,1.20623164165363,2.285749791587));
#53731=CARTESIAN_POINT('Ctrl Pts',(-8.22859457440256,0.408071081466186,
2.42032064888589));
#53732=CARTESIAN_POINT('Ctrl Pts',(-8.1863472014693,-0.390089478721252,
2.55489150618479));
#53733=CARTESIAN_POINT('Ctrl Pts',(-8.14409982853603,-1.26136728339215,
2.25579257132536));
#53734=CARTESIAN_POINT('Ctrl Pts',(-8.10185245560277,-1.80858426161825,
1.65936788193681));
#53735=CARTESIAN_POINT('Ctrl Pts',(-8.07034413580586,-2.21670165096406,
1.21455111480413));
#53736=CARTESIAN_POINT('Ctrl Pts',(-8.03883581600897,-2.44456807139402,
0.604354113579378));
#53737=CARTESIAN_POINT('Ctrl Pts',(-8.00732749621207,-2.44998306124988,
-0.00220861612412772));
#53738=CARTESIAN_POINT('Origin',(-4.85,0.,0.));
#53739=CARTESIAN_POINT('',(-7.09167250378795,-2.45424633052781,0.000682524973613097));
#53740=CARTESIAN_POINT('',(-7.20732749621206,-2.45412426038782,0.000841066407299921));
#53741=CARTESIAN_POINT('',(-4.85,-2.4505,-3.00099698131059E-16));
#53742=CARTESIAN_POINT('Ctrl Pts',(-7.09167250378795,-2.45424633052781,
0.000682524973613097));
#53743=CARTESIAN_POINT('Ctrl Pts',(-7.09363455345465,-2.45438587279557,
0.0382834665408473));
#53744=CARTESIAN_POINT('Ctrl Pts',(-7.09559660312136,-2.4535962127551,0.0758784207214286));
#53745=CARTESIAN_POINT('Ctrl Pts',(-7.09755865278807,-2.45185899785181,
0.113429538489877));
#53746=CARTESIAN_POINT('Ctrl Pts',(-7.13980602572134,-2.41445282657598,
0.921990149030203));
#53747=CARTESIAN_POINT('Ctrl Pts',(-7.1820533986546,-1.93772380966174,1.71022651442513));
#53748=CARTESIAN_POINT('Ctrl Pts',(-7.22430077158786,-1.23899271099641,
2.11881473280963));
#53749=CARTESIAN_POINT('Ctrl Pts',(-7.26654814452113,-0.540261612331091,
2.52740295119414));
#53750=CARTESIAN_POINT('Ctrl Pts',(-7.30879551745439,0.3804715680853,2.55634302256822));
#53751=CARTESIAN_POINT('Ctrl Pts',(-7.35104289038765,1.10348319354511,2.19244239041122));
#53752=CARTESIAN_POINT('Ctrl Pts',(-7.39329026332091,1.82649481900493,1.82854175825421));
#53753=CARTESIAN_POINT('Ctrl Pts',(-7.43553763625417,2.35178488950816,1.07180042256612));
#53754=CARTESIAN_POINT('Ctrl Pts',(-7.47778500918743,2.4398956916372,0.267185002312099));
#53755=CARTESIAN_POINT('Ctrl Pts',(-7.5200323821207,2.52800649376624,-0.537430417941909));
#53756=CARTESIAN_POINT('Ctrl Pts',(-7.56227975505396,2.17893802752108,-1.38991992276184));
#53757=CARTESIAN_POINT('Ctrl Pts',(-7.60452712798722,1.55181597081934,-1.90166927357545));
#53758=CARTESIAN_POINT('Ctrl Pts',(-7.64677450092048,0.924693914117586,
-2.41341862438908));
#53759=CARTESIAN_POINT('Ctrl Pts',(-7.68902187385375,0.0195182669592417,
-2.58442782119639));
#53760=CARTESIAN_POINT('Ctrl Pts',(-7.73126924678701,-0.751079369498862,
-2.33674100060766));
#53761=CARTESIAN_POINT('Ctrl Pts',(-7.77351661972027,-1.52167700595696,
-2.08905418001893));
#53762=CARTESIAN_POINT('Ctrl Pts',(-7.81576399265353,-2.15769663171482,
-1.42267134203417));
#53763=CARTESIAN_POINT('Ctrl Pts',(-7.85801136558679,-2.36920355695109,
-0.641368363882281));
#53764=CARTESIAN_POINT('Ctrl Pts',(-7.86923174498718,-2.42537717869814,
-0.433863962239076));
#53765=CARTESIAN_POINT('Ctrl Pts',(-7.88045212438756,-2.45160703890997,
-0.218253463255248));
#53766=CARTESIAN_POINT('Ctrl Pts',(-7.89167250378795,-2.44971218776673,
-0.00219053278463388));
#53767=CARTESIAN_POINT('Ctrl Pts',(-8.00732749621207,-2.44998306124988,
-0.00220861612412772));
#53768=CARTESIAN_POINT('Ctrl Pts',(-7.99658844307571,-2.45182866470223,
-0.208944786977084));
#53769=CARTESIAN_POINT('Ctrl Pts',(-7.98584938993934,-2.42783282903302,
-0.415258776655366));
#53770=CARTESIAN_POINT('Ctrl Pts',(-7.97511033680298,-2.37632469663013,
-0.614458734829266));
#53771=CARTESIAN_POINT('Ctrl Pts',(-7.93286296386972,-2.17369200163464,
-1.3981102182891));
#53772=CARTESIAN_POINT('Ctrl Pts',(-7.89061559093646,-1.54527045986237,
-2.07166274129109));
#53773=CARTESIAN_POINT('Ctrl Pts',(-7.8483682180032,-0.777531351301464,
-2.32807268057354));
#53774=CARTESIAN_POINT('Ctrl Pts',(-7.80612084506993,-0.00979224274055196,
-2.58448261985599));
#53775=CARTESIAN_POINT('Ctrl Pts',(-7.76387347213667,0.897264432609006,
-2.42374997541889));
#53776=CARTESIAN_POINT('Ctrl Pts',(-7.72162609920341,1.53014971651881,-1.91914564019643));
#53777=CARTESIAN_POINT('Ctrl Pts',(-7.67937872627014,2.16303500042861,-1.41454130497397));
#53778=CARTESIAN_POINT('Ctrl Pts',(-7.63713135333688,2.52174889289865,-0.566065278966143));
#53779=CARTESIAN_POINT('Ctrl Pts',(-7.59488398040362,2.44276870532455,0.239497607437949));
#53780=CARTESIAN_POINT('Ctrl Pts',(-7.55263660747036,2.36378851775044,1.04506049384204));
#53781=CARTESIAN_POINT('Ctrl Pts',(-7.5103892345371,1.84711425013217,1.80771024064241));
#53782=CARTESIAN_POINT('Ctrl Pts',(-7.46814186160384,1.12827606704126,2.17978692041014));
#53783=CARTESIAN_POINT('Ctrl Pts',(-7.42589448867057,0.409437883950348,
2.55186360017788));
#53784=CARTESIAN_POINT('Ctrl Pts',(-7.38364711573731,-0.511564214613206,
2.533367212913));
#53785=CARTESIAN_POINT('Ctrl Pts',(-7.34139974280405,-1.21488402143036,
2.13272943126949));
#53786=CARTESIAN_POINT('Ctrl Pts',(-7.29915236987079,-1.91820382824751,
1.73209164962598));
#53787=CARTESIAN_POINT('Ctrl Pts',(-7.25690499693752,-2.40384134331826,
0.949312473603835));
#53788=CARTESIAN_POINT('Ctrl Pts',(-7.21465762400426,-2.45041478266452,
0.141228125619655));
#53789=CARTESIAN_POINT('Ctrl Pts',(-7.21221424807353,-2.45310835655585,
0.0944925842408962));
#53790=CARTESIAN_POINT('Ctrl Pts',(-7.20977087214279,-2.45433331169064,
0.0476723999768843));
#53791=CARTESIAN_POINT('Ctrl Pts',(-7.20732749621206,-2.45412426038782,
0.000841066407299921));
#53792=CARTESIAN_POINT('Origin',(-4.85,0.,0.));
#53793=CARTESIAN_POINT('',(-6.29167250378795,-2.44778349460883,0.00166651518545433));
#53794=CARTESIAN_POINT('',(-6.40732749621207,-2.44759559891841,0.00156187491458784));
#53795=CARTESIAN_POINT('',(-4.85,-2.4505,-3.00099698131059E-16));
#53796=CARTESIAN_POINT('Ctrl Pts',(-6.29167250378795,-2.44778349460883,
0.00166651518545433));
#53797=CARTESIAN_POINT('Ctrl Pts',(-6.30681698252175,-2.44962168320389,
0.293874483510101));
#53798=CARTESIAN_POINT('Ctrl Pts',(-6.32196146125555,-2.40122185351473,
0.585493705442811));
#53799=CARTESIAN_POINT('Ctrl Pts',(-6.33710593998935,-2.29986782320631,
0.857372031787032));
#53800=CARTESIAN_POINT('Ctrl Pts',(-6.37935331292261,-2.01712837789465,
1.61580982601093));
#53801=CARTESIAN_POINT('Ctrl Pts',(-6.42160068585587,-1.32229978843967,
2.22062413668589));
#53802=CARTESIAN_POINT('Ctrl Pts',(-6.46384805878913,-0.532125265238115,
2.39610548752291));
#53803=CARTESIAN_POINT('Ctrl Pts',(-6.5060954317224,0.258049257963456,2.57158683835993));
#53804=CARTESIAN_POINT('Ctrl Pts',(-6.54834280465566,1.14356971491161,2.31773522935899));
#53805=CARTESIAN_POINT('Ctrl Pts',(-6.59059017758893,1.72076447115239,1.75027096180509));
#53806=CARTESIAN_POINT('Ctrl Pts',(-6.63283755052219,2.29795922739315,1.1828066942512));
#53807=CARTESIAN_POINT('Ctrl Pts',(-6.67508492345545,2.56682828292656,0.301729768144353));
#53808=CARTESIAN_POINT('Ctrl Pts',(-6.71733229638871,2.40480551258969,-0.491313801687984));
#53809=CARTESIAN_POINT('Ctrl Pts',(-6.75957966932197,2.24278274225283,-1.28435737152033));
#53810=CARTESIAN_POINT('Ctrl Pts',(-6.80182704225524,1.64986814604569,-1.98936758507816));
#53811=CARTESIAN_POINT('Ctrl Pts',(-6.8440744151885,0.896346619568618,-2.28495985598806));
#53812=CARTESIAN_POINT('Ctrl Pts',(-6.88632178812176,0.142825093091551,
-2.58055212689795));
#53813=CARTESIAN_POINT('Ctrl Pts',(-6.92856916105502,-0.771303363655447,
-2.46672645515992));
#53814=CARTESIAN_POINT('Ctrl Pts',(-6.97081653398828,-1.42932592921024,
-1.99537119144805));
#53815=CARTESIAN_POINT('Ctrl Pts',(-7.01110185725484,-2.05678865480829,
-1.54590657735191));
#53816=CARTESIAN_POINT('Ctrl Pts',(-7.05138718052139,-2.45138121173831,
-0.771349963227231));
#53817=CARTESIAN_POINT('Ctrl Pts',(-7.09167250378795,-2.45424633052781,
0.000682524973613097));
#53818=CARTESIAN_POINT('Ctrl Pts',(-7.20732749621206,-2.45412426038782,
0.000841066407299921));
#53819=CARTESIAN_POINT('Ctrl Pts',(-7.16752349920953,-2.45071869461871,
-0.762068249994661));
#53820=CARTESIAN_POINT('Ctrl Pts',(-7.127719502207,-2.06675247208674,-1.52793640042953));
#53821=CARTESIAN_POINT('Ctrl Pts',(-7.08791550520447,-1.4518628975676,-1.97903312234382));
#53822=CARTESIAN_POINT('Ctrl Pts',(-7.04566813227121,-0.799228209502633,
-2.45782050237689));
#53823=CARTESIAN_POINT('Ctrl Pts',(-7.00342075933795,0.113550530249083,
-2.58200574249679));
#53824=CARTESIAN_POINT('Ctrl Pts',(-6.96117338640468,0.870375782186031,
-2.29497799264066));
#53825=CARTESIAN_POINT('Ctrl Pts',(-6.91892601347142,1.62720103412297,-2.00795024278453));
#53826=CARTESIAN_POINT('Ctrl Pts',(-6.87667864053816,2.22807279824515,-1.30970950295236));
#53827=CARTESIAN_POINT('Ctrl Pts',(-6.8344312676049,2.3990788384909,-0.518554443884578));
#53828=CARTESIAN_POINT('Ctrl Pts',(-6.79218389467164,2.57008487873666,0.272600615183211));
#53829=CARTESIAN_POINT('Ctrl Pts',(-6.74993652173838,2.31122519510601,1.15666999348662));
#53830=CARTESIAN_POINT('Ctrl Pts',(-6.70768914880512,1.74050306065297,1.73064354459267));
#53831=CARTESIAN_POINT('Ctrl Pts',(-6.66544177587185,1.16978092619992,2.30461709569873));
#53832=CARTESIAN_POINT('Ctrl Pts',(-6.62319440293859,0.287196340924479,
2.56849481960743));
#53833=CARTESIAN_POINT('Ctrl Pts',(-6.58094703000532,-0.504917401848296,
2.40198592881454));
#53834=CARTESIAN_POINT('Ctrl Pts',(-6.53869965707206,-1.29703114462107,
2.23547703802164));
#53835=CARTESIAN_POINT('Ctrl Pts',(-6.4964522841388,-1.99867404489118,1.63858153252716));
#53836=CARTESIAN_POINT('Ctrl Pts',(-6.45420491120554,-2.28999653358123,
0.883399037985938));
#53837=CARTESIAN_POINT('Ctrl Pts',(-6.43857910620771,-2.39774639076035,
0.604083814856844));
#53838=CARTESIAN_POINT('Ctrl Pts',(-6.42295330120989,-2.44936450788483,
0.30311496721273));
#53839=CARTESIAN_POINT('Ctrl Pts',(-6.40732749621207,-2.44759559891841,
0.00156187491458784));
#53840=CARTESIAN_POINT('Origin',(-4.85,0.,0.));
#53841=CARTESIAN_POINT('',(-5.49167250378794,-2.44831607326794,-0.00189653782627697));
#53842=CARTESIAN_POINT('',(-5.60732749621207,-2.44854493522231,-0.00197153692530977));
#53843=CARTESIAN_POINT('',(-4.85,-2.4505,-3.00099698131059E-16));
#53844=CARTESIAN_POINT('Ctrl Pts',(-5.49167250378794,-2.44831607326794,
-0.00189653782627697));
#53845=CARTESIAN_POINT('Ctrl Pts',(-5.51999941158884,-2.44434671486883,
0.544362953986012));
#53846=CARTESIAN_POINT('Ctrl Pts',(-5.54832631938974,-2.26370630972924,
1.0930041977374));
#53847=CARTESIAN_POINT('Ctrl Pts',(-5.57665322719063,-1.92777581339653,
1.51926272198234));
#53848=CARTESIAN_POINT('Ctrl Pts',(-5.61890060012389,-1.42676168725263,
2.15499405440788));
#53849=CARTESIAN_POINT('Ctrl Pts',(-5.66114797305715,-0.580329673604588,
2.5185046667982));
#53850=CARTESIAN_POINT('Ctrl Pts',(-5.70339534599041,0.225667374856916,
2.44408531787464));
#53851=CARTESIAN_POINT('Ctrl Pts',(-5.74564271892368,1.03166442331841,2.36966596895107));
#53852=CARTESIAN_POINT('Ctrl Pts',(-5.78789009185694,1.79722650659338,1.85731665871363));
#53853=CARTESIAN_POINT('Ctrl Pts',(-5.8301374647902,2.17336598128022,1.14059594797335));
#53854=CARTESIAN_POINT('Ctrl Pts',(-5.87238483772346,2.54950545596706,0.423875237233074));
#53855=CARTESIAN_POINT('Ctrl Pts',(-5.91463221065673,2.53622232206579,-0.497216874010042));
#53856=CARTESIAN_POINT('Ctrl Pts',(-5.95687958358999,2.13957180317949,-1.2027931260855));
#53857=CARTESIAN_POINT('Ctrl Pts',(-5.99912695652325,1.7429212842932,-1.90836937816096));
#53858=CARTESIAN_POINT('Ctrl Pts',(-6.04137432945651,0.96290338042188,-2.39842977106876));
#53859=CARTESIAN_POINT('Ctrl Pts',(-6.08362170238978,0.155095537252022,
-2.44957632652366));
#53860=CARTESIAN_POINT('Ctrl Pts',(-6.12586907532304,-0.65271230591783,
-2.50072288197856));
#53861=CARTESIAN_POINT('Ctrl Pts',(-6.1681164482563,-1.48831008838622,-2.11295559998057));
#53862=CARTESIAN_POINT('Ctrl Pts',(-6.21036382118956,-1.97078382903626,
-1.46304132009516));
#53863=CARTESIAN_POINT('Ctrl Pts',(-6.23746671538902,-2.28030448887734,
-1.04610278064375));
#53864=CARTESIAN_POINT('Ctrl Pts',(-6.26456960958849,-2.4444938316309,-0.521275329756746));
#53865=CARTESIAN_POINT('Ctrl Pts',(-6.29167250378795,-2.44778349460883,
0.00166651518545433));
#53866=CARTESIAN_POINT('Ctrl Pts',(-6.40732749621207,-2.44759559891841,
0.00156187491458784));
#53867=CARTESIAN_POINT('Ctrl Pts',(-6.38070592827663,-2.44458192184847,
-0.512191889059406));
#53868=CARTESIAN_POINT('Ctrl Pts',(-6.35408436034119,-2.2866087506118,-1.02764146309601));
#53869=CARTESIAN_POINT('Ctrl Pts',(-6.32746279240576,-1.98724892687709,
-1.44059698964044));
#53870=CARTESIAN_POINT('Ctrl Pts',(-6.28521541947249,-1.51217675437289,
-2.09594103913763));
#53871=CARTESIAN_POINT('Ctrl Pts',(-6.24296804653923,-0.681030332254514,
-2.49315965454405));
#53872=CARTESIAN_POINT('Ctrl Pts',(-6.20072067360596,0.127305546892975,
-2.45117752967657));
#53873=CARTESIAN_POINT('Ctrl Pts',(-6.1584733006727,0.935641426040468,-2.40919540480908));
#53874=CARTESIAN_POINT('Ctrl Pts',(-6.11622592773944,1.72116676221708,-1.92801253966767));
#53875=CARTESIAN_POINT('Ctrl Pts',(-6.07397855480618,2.1257935023211,-1.22698002005643));
#53876=CARTESIAN_POINT('Ctrl Pts',(-6.03173118187292,2.53042024242512,-0.525947500445177));
#53877=CARTESIAN_POINT('Ctrl Pts',(-5.98948380893965,2.55414838645656,0.394934673635915));
#53878=CARTESIAN_POINT('Ctrl Pts',(-5.94723643600639,2.18616126880922,1.11587494410122));
#53879=CARTESIAN_POINT('Ctrl Pts',(-5.90498906307313,1.81817415116189,1.83681521456651));
#53880=CARTESIAN_POINT('Ctrl Pts',(-5.86274169013987,1.05847177183578,2.35781358141602));
#53881=CARTESIAN_POINT('Ctrl Pts',(-5.8204943172066,0.253370580970988,2.44136874168104));
#53882=CARTESIAN_POINT('Ctrl Pts',(-5.77824694427334,-0.551730609893816,
2.52492390194606));
#53883=CARTESIAN_POINT('Ctrl Pts',(-5.73599957134008,-1.40223061229731,
2.17103585562659));
#53884=CARTESIAN_POINT('Ctrl Pts',(-5.69375219840682,-1.91042214809686,
1.5410273197443));
#53885=CARTESIAN_POINT('Ctrl Pts',(-5.6649439643419,-2.25695495467515,1.11142822033371));
#53886=CARTESIAN_POINT('Ctrl Pts',(-5.63613573027698,-2.44432132291076,
0.553438738665929));
#53887=CARTESIAN_POINT('Ctrl Pts',(-5.60732749621207,-2.44854493522231,
-0.00197153692530977));
#53888=CARTESIAN_POINT('Origin',(-4.85,0.,0.));
#53889=CARTESIAN_POINT('',(-4.69167250378794,-2.45444635238797,-0.00026109281808101));
#53890=CARTESIAN_POINT('',(-4.80732749621206,-2.45447688366933,-9.10453097679518E-5));
#53891=CARTESIAN_POINT('',(-4.85,-2.4505,-3.00099698131059E-16));
#53892=CARTESIAN_POINT('Ctrl Pts',(-4.69167250378794,-2.45444635238797,
-0.00026109281808101));
#53893=CARTESIAN_POINT('Ctrl Pts',(-4.73318184065593,-2.45323838965266,
0.795054750259954));
#53894=CARTESIAN_POINT('Ctrl Pts',(-4.77469117752392,-2.03080581207006,
1.59147263731996));
#53895=CARTESIAN_POINT('Ctrl Pts',(-4.81620051439191,-1.37119273741817,
2.03575766779202));
#53896=CARTESIAN_POINT('Ctrl Pts',(-4.85844788732517,-0.699851741412878,
2.48794208670272));
#53897=CARTESIAN_POINT('Ctrl Pts',(-4.90069526025843,0.217178870277101,
2.57536048448576));
#53898=CARTESIAN_POINT('Ctrl Pts',(-4.94294263319169,0.961863305267408,
2.25816248022647));
#53899=CARTESIAN_POINT('Ctrl Pts',(-4.98519000612495,1.70654774025772,1.94096447596719));
#53900=CARTESIAN_POINT('Ctrl Pts',(-5.02743737905822,2.27888599854835,1.21915006966559));
#53901=CARTESIAN_POINT('Ctrl Pts',(-5.06968475199148,2.41797307406147,0.421764173723033));
#53902=CARTESIAN_POINT('Ctrl Pts',(-5.11193212492474,2.55706014957458,-0.375621722219518));
#53903=CARTESIAN_POINT('Ctrl Pts',(-5.154179497858,2.26289604231019,-1.24857910780302));
#53904=CARTESIAN_POINT('Ctrl Pts',(-5.19642687079127,1.66957783049421,-1.79916332583916));
#53905=CARTESIAN_POINT('Ctrl Pts',(-5.23867424372453,1.07625961867823,-2.34974754387529));
#53906=CARTESIAN_POINT('Ctrl Pts',(-5.28092161665779,0.183787302310668,
-2.57795859436406));
#53907=CARTESIAN_POINT('Ctrl Pts',(-5.32316898959106,-0.600998423000285,
-2.37976463136043));
#53908=CARTESIAN_POINT('Ctrl Pts',(-5.36541636252432,-1.38578414831124,
-2.1815706683568));
#53909=CARTESIAN_POINT('Ctrl Pts',(-5.40766373545758,-2.06288328256559,
-1.55697169186076));
#53910=CARTESIAN_POINT('Ctrl Pts',(-5.44991110839084,-2.32363473037289,
-0.790696177382358));
#53911=CARTESIAN_POINT('Ctrl Pts',(-5.46383157352321,-2.40955205931899,
-0.538209197944985));
#53912=CARTESIAN_POINT('Ctrl Pts',(-5.47775203865557,-2.45026670323366,
-0.270340459148239));
#53913=CARTESIAN_POINT('Ctrl Pts',(-5.49167250378794,-2.44831607326794,
-0.00189653782627697));
#53914=CARTESIAN_POINT('Ctrl Pts',(-5.60732749621207,-2.44854493522231,
-0.00197153692530977));
#53915=CARTESIAN_POINT('Ctrl Pts',(-5.59388835734372,-2.45051526468621,
-0.261072313660039));
#53916=CARTESIAN_POINT('Ctrl Pts',(-5.58044921847538,-2.41262907617418,
-0.519611789606023));
#53917=CARTESIAN_POINT('Ctrl Pts',(-5.56701007960703,-2.33245222215829,
-0.764293540131167));
#53918=CARTESIAN_POINT('Ctrl Pts',(-5.52476270667377,-2.08040769122459,
-1.53347683867927));
#53919=CARTESIAN_POINT('Ctrl Pts',(-5.4825153337405,-1.41043556016157,-2.1657144103304));
#53920=CARTESIAN_POINT('Ctrl Pts',(-5.44026796080724,-0.627948022535169,
-2.37279566442992));
#53921=CARTESIAN_POINT('Ctrl Pts',(-5.39802058787398,0.154539515091236,
-2.57987691852945));
#53922=CARTESIAN_POINT('Ctrl Pts',(-5.35577321494072,1.04954245928102,-2.36180185507737));
#53923=CARTESIAN_POINT('Ctrl Pts',(-5.31352584200746,1.64906650734465,-1.81798174866911));
#53924=CARTESIAN_POINT('Ctrl Pts',(-5.2712784690742,2.24859055540828,-1.27416164226085));
#53925=CARTESIAN_POINT('Ctrl Pts',(-5.22903109614093,2.55263570734576,-0.404596492896413));
#53926=CARTESIAN_POINT('Ctrl Pts',(-5.18678372320767,2.42260053111077,0.394315420446647));
#53927=CARTESIAN_POINT('Ctrl Pts',(-5.1445363502744,2.29256535487578,1.19322733378971));
#53928=CARTESIAN_POINT('Ctrl Pts',(-5.10228897734114,1.72844985046831,1.9214860111114));
#53929=CARTESIAN_POINT('Ctrl Pts',(-5.06004160440788,0.987410615361824,
2.24710886714723));
#53930=CARTESIAN_POINT('Ctrl Pts',(-5.01779423147462,0.246371380255345,
2.57273172318307));
#53931=CARTESIAN_POINT('Ctrl Pts',(-4.97554685854136,-0.671591585550147,
2.49571875793305));
#53932=CARTESIAN_POINT('Ctrl Pts',(-4.9332994856081,-1.34801746853503,2.05117695206065));
#53933=CARTESIAN_POINT('Ctrl Pts',(-4.89130882247608,-2.02033315147846,
1.60933633754549));
#53934=CARTESIAN_POINT('Ctrl Pts',(-4.84931815934407,-2.45403816100393,
0.8044197798363));
#53935=CARTESIAN_POINT('Ctrl Pts',(-4.80732749621206,-2.45447688366933,
-9.10453097679518E-5));
#53936=CARTESIAN_POINT('Origin',(-4.85,0.,0.));
#53937=CARTESIAN_POINT('',(-3.89167250378794,-2.44904833524983,0.00209640718090015));
#53938=CARTESIAN_POINT('',(-4.00732749621206,-2.4487999781993,0.00204119660086303));
#53939=CARTESIAN_POINT('',(-4.85,-2.4505,-3.00099698131059E-16));
#53940=CARTESIAN_POINT('Ctrl Pts',(-3.89167250378794,-2.44904833524983,
0.00209640718090015));
#53941=CARTESIAN_POINT('Ctrl Pts',(-3.90411689678976,-2.45101740052764,
0.241894248235633));
#53942=CARTESIAN_POINT('Ctrl Pts',(-3.91656128979158,-2.41863571201545,
0.481171829065209));
#53943=CARTESIAN_POINT('Ctrl Pts',(-3.9290056827934,-2.34972373355784,0.709420313421929));
#53944=CARTESIAN_POINT('Ctrl Pts',(-3.97125305572666,-2.11577499431097,
1.48429931625169));
#53945=CARTESIAN_POINT('Ctrl Pts',(-4.01350042865992,-1.46080395431589,
2.13206474896982));
#53946=CARTESIAN_POINT('Ctrl Pts',(-4.05574780159318,-0.68338443893331,
2.35742752035839));
#53947=CARTESIAN_POINT('Ctrl Pts',(-4.09799517452644,0.0940350764492678,
2.58279029174695));
#53948=CARTESIAN_POINT('Ctrl Pts',(-4.14024254745971,0.993903067219349,
2.38575040180594));
#53949=CARTESIAN_POINT('Ctrl Pts',(-4.18248992039297,1.60600746001602,1.856130071814));
#53950=CARTESIAN_POINT('Ctrl Pts',(-4.22473729332624,2.21811185281269,1.32650974182207));
#53951=CARTESIAN_POINT('Ctrl Pts',(-4.26698466625949,2.54245264763596,0.464308971779215));
#53952=CARTESIAN_POINT('Ctrl Pts',(-4.30923203919276,2.43117648011452,-0.337431070980653));
#53953=CARTESIAN_POINT('Ctrl Pts',(-4.35147941212602,2.31990031259309,-1.13917111374053));
#53954=CARTESIAN_POINT('Ctrl Pts',(-4.39372678505928,1.77300718272696,-1.8804504292174));
#53955=CARTESIAN_POINT('Ctrl Pts',(-4.43597415799255,1.0398027298051,-2.22335086934377));
#53956=CARTESIAN_POINT('Ctrl Pts',(-4.47822153092581,0.306598276883252,
-2.56625130947013));
#53957=CARTESIAN_POINT('Ctrl Pts',(-4.52046890385907,-0.612917499094324,
-2.51077287424597));
#53958=CARTESIAN_POINT('Ctrl Pts',(-4.56271627679233,-1.29957592358191,
-2.08220585532948));
#53959=CARTESIAN_POINT('Ctrl Pts',(-4.60496364972559,-1.98623434806949,
-1.65363883641299));
#53960=CARTESIAN_POINT('Ctrl Pts',(-4.64721102265886,-2.44003542106709,
-0.851983233804166));
#53961=CARTESIAN_POINT('Ctrl Pts',(-4.68945839559212,-2.45411026740558,
-0.0426802124805824));
#53962=CARTESIAN_POINT('Ctrl Pts',(-4.69019643165739,-2.45435614646243,
-0.0285421779472637));
#53963=CARTESIAN_POINT('Ctrl Pts',(-4.69093446772267,-2.45446782996703,
-0.0144018095763991));
#53964=CARTESIAN_POINT('Ctrl Pts',(-4.69167250378794,-2.45444635238797,
-0.00026109281808101));
#53965=CARTESIAN_POINT('Ctrl Pts',(-4.80732749621206,-2.45447688366933,
-9.10453097679518E-5));
#53966=CARTESIAN_POINT('Ctrl Pts',(-4.80707078641081,-2.45447956579912,
-0.00500941998221655));
#53967=CARTESIAN_POINT('Ctrl Pts',(-4.80681407660956,-2.45446605466731,
-0.00992777949047233));
#53968=CARTESIAN_POINT('Ctrl Pts',(-4.80655736680831,-2.45443630579685,
-0.0148460407822334));
#53969=CARTESIAN_POINT('Ctrl Pts',(-4.76430999387504,-2.44954045990948,
-0.824256581257921));
#53970=CARTESIAN_POINT('Ctrl Pts',(-4.72206262094178,-2.00485996797048,
-1.63100701571451));
#53971=CARTESIAN_POINT('Ctrl Pts',(-4.67981524800852,-1.32310601479308,
-2.06733365903014));
#53972=CARTESIAN_POINT('Ctrl Pts',(-4.63756787507526,-0.641352061615665,
-2.50366030234578));
#53973=CARTESIAN_POINT('Ctrl Pts',(-4.59532050214199,0.277475352800151,
-2.56956315452044));
#53974=CARTESIAN_POINT('Ctrl Pts',(-4.55307312920873,1.01452134907151,-2.23499986944486));
#53975=CARTESIAN_POINT('Ctrl Pts',(-4.51082575627547,1.75156734534285,-1.9004365843693));
#53976=CARTESIAN_POINT('Ctrl Pts',(-4.46857838334221,2.30683192346974,-1.16540716204352));
#53977=CARTESIAN_POINT('Ctrl Pts',(-4.42633101040895,2.42719325203068,-0.364980686389968));
#53978=CARTESIAN_POINT('Ctrl Pts',(-4.38408363747569,2.54755458059162,0.435445789263594));
#53979=CARTESIAN_POINT('Ctrl Pts',(-4.34183626454242,2.23301265958659,1.30126931824493));
#53980=CARTESIAN_POINT('Ctrl Pts',(-4.29958889160916,1.62695395780928,1.83779726937138));
#53981=CARTESIAN_POINT('Ctrl Pts',(-4.2573415186759,1.02089525603198,2.37432522049783));
#53982=CARTESIAN_POINT('Ctrl Pts',(-4.21509414574264,0.123319773482412,
2.5815575937694));
#53983=CARTESIAN_POINT('Ctrl Pts',(-4.17284677280938,-0.656605474814574,
2.36502584226545));
#53984=CARTESIAN_POINT('Ctrl Pts',(-4.13059939987611,-1.43653072311158,
2.1484940907615));
#53985=CARTESIAN_POINT('Ctrl Pts',(-4.08835202694285,-2.09880573715599,
1.50819821448203));
#53986=CARTESIAN_POINT('Ctrl Pts',(-4.04610465400958,-2.34152711618347,
0.736022247164297));
#53987=CARTESIAN_POINT('Ctrl Pts',(-4.03317893474374,-2.41578850067437,
0.499772533054371));
#53988=CARTESIAN_POINT('Ctrl Pts',(-4.0202532154779,-2.45077657478841,0.251177871086556));
#53989=CARTESIAN_POINT('Ctrl Pts',(-4.00732749621206,-2.4487999781993,0.00204119660086303));
#53990=CARTESIAN_POINT('Origin',(-4.85,0.,0.));
#53991=CARTESIAN_POINT('',(-3.09167250378794,-2.44725071792797,-0.00132331670171071));
#53992=CARTESIAN_POINT('',(-3.20732749621206,-2.44741005262324,-0.00144229910683621));
#53993=CARTESIAN_POINT('',(-4.85,-2.4505,-3.00099698131059E-16));
#53994=CARTESIAN_POINT('Ctrl Pts',(-3.09167250378794,-2.44725071792797,
-0.00132331670171071));
#53995=CARTESIAN_POINT('Ctrl Pts',(-3.11729932585685,-2.44481399137148,
0.493408423386824));
#53996=CARTESIAN_POINT('Ctrl Pts',(-3.14292614792576,-2.29924344722054,
0.989458790886426));
#53997=CARTESIAN_POINT('Ctrl Pts',(-3.16855296999468,-2.02046507845012,
1.39362824047613));
#53998=CARTESIAN_POINT('Ctrl Pts',(-3.21080034292794,-1.5608820025814,2.05992613020793));
#53999=CARTESIAN_POINT('Ctrl Pts',(-3.2530477158612,-0.739273023463133,
2.47651442222843));
#54000=CARTESIAN_POINT('Ctrl Pts',(-3.29529508879446,0.0698247858651539,
2.45348798741501));
#54001=CARTESIAN_POINT('Ctrl Pts',(-3.33754246172772,0.878922595193441,
2.4304615526016));
#54002=CARTESIAN_POINT('Ctrl Pts',(-3.37978983466098,1.67550923473175,1.96782039095427));
#54003=CARTESIAN_POINT('Ctrl Pts',(-3.42203720759425,2.09645426748447,1.27646320325523));
#54004=CARTESIAN_POINT('Ctrl Pts',(-3.46428458052751,2.5173993002372,0.585106015556197));
#54005=CARTESIAN_POINT('Ctrl Pts',(-3.50653195346077,2.56270272620434,-0.334967198194552));
#54006=CARTESIAN_POINT('Ctrl Pts',(-3.54877932639404,2.21171261350024,-1.06433365094129));
#54007=CARTESIAN_POINT('Ctrl Pts',(-3.5910266993273,1.86072250079615,-1.79370010368804));
#54008=CARTESIAN_POINT('Ctrl Pts',(-3.63327407226056,1.11343884942081,-2.33235979543077));
#54009=CARTESIAN_POINT('Ctrl Pts',(-3.67552144519382,0.310516932425231,
-2.43476036598832));
#54010=CARTESIAN_POINT('Ctrl Pts',(-3.71776881812708,-0.492404984570358,
-2.53716093654587));
#54011=CARTESIAN_POINT('Ctrl Pts',(-3.76001619106035,-1.35096516718619,
-2.20330238591822));
#54012=CARTESIAN_POINT('Ctrl Pts',(-3.80226356399361,-1.87378203924477,
-1.58537682413371));
#54013=CARTESIAN_POINT('Ctrl Pts',(-3.83206654392505,-2.24259788894024,
-1.14946751573524));
#54014=CARTESIAN_POINT('Ctrl Pts',(-3.8618695238565,-2.44433263614344,-0.572193575746662));
#54015=CARTESIAN_POINT('Ctrl Pts',(-3.89167250378794,-2.44904833524983,
0.00209640718090015));
#54016=CARTESIAN_POINT('Ctrl Pts',(-4.00732749621206,-2.4487999781993,0.00204119660086303));
#54017=CARTESIAN_POINT('Ctrl Pts',(-3.97800584254464,-2.44431612090407,
-0.563118786753198));
#54018=CARTESIAN_POINT('Ctrl Pts',(-3.94868418887722,-2.24961307590875,
-1.1310679517478));
#54019=CARTESIAN_POINT('Ctrl Pts',(-3.9193625352098,-1.89164075675834,-1.56402469018496));
#54020=CARTESIAN_POINT('Ctrl Pts',(-3.87711516227654,-1.37586527429514,
-2.18783960186053));
#54021=CARTESIAN_POINT('Ctrl Pts',(-3.83486778934327,-0.521146565358179,
-2.5314133668557));
#54022=CARTESIAN_POINT('Ctrl Pts',(-3.79262041641001,0.282884960559793,
-2.43812511640121));
#54023=CARTESIAN_POINT('Ctrl Pts',(-3.75037304347675,1.08691648647776,-2.34483686594671));
#54024=CARTESIAN_POINT('Ctrl Pts',(-3.70812567054349,1.84026082937673,-1.81468660004255));
#54025=CARTESIAN_POINT('Ctrl Pts',(-3.66587829761023,2.19949990122418,-1.08934758854723));
#54026=CARTESIAN_POINT('Ctrl Pts',(-3.62363092467696,2.55873897307164,-0.364008577051898));
#54027=CARTESIAN_POINT('Ctrl Pts',(-3.5813835517437,2.52387277386756,0.55651918003457));
#54028=CARTESIAN_POINT('Ctrl Pts',(-3.53913617881044,2.11079534144264,1.25260568841855));
#54029=CARTESIAN_POINT('Ctrl Pts',(-3.49688880587718,1.69771790901772,1.94869219680253));
#54030=CARTESIAN_POINT('Ctrl Pts',(-3.45464143294391,0.906429243371915,
2.42033745648402));
#54031=CARTESIAN_POINT('Ctrl Pts',(-3.41239406001065,0.0976446577005888,
2.45253817604351));
#54032=CARTESIAN_POINT('Ctrl Pts',(-3.37014668707739,-0.71113992797075,
2.48473889560299));
#54033=CARTESIAN_POINT('Ctrl Pts',(-3.32789931414413,-1.53742043366764,
2.07749507504048));
#54034=CARTESIAN_POINT('Ctrl Pts',(-3.28565194121086,-2.00453023386089,
1.41645209089424));
#54035=CARTESIAN_POINT('Ctrl Pts',(-3.25954379287793,-2.29319603967271,
1.00793891986703));
#54036=CARTESIAN_POINT('Ctrl Pts',(-3.23343564454499,-2.44469358413537,
0.502499163605551));
#54037=CARTESIAN_POINT('Ctrl Pts',(-3.20732749621206,-2.44741005262324,
-0.00144229910683621));
#54038=CARTESIAN_POINT('Origin',(-4.85,0.,0.));
#54039=CARTESIAN_POINT('',(-2.29167250378794,-2.45380537632986,-0.00115034636150174));
#54040=CARTESIAN_POINT('',(-2.40732749621206,-2.45397025608505,-0.00100410518415028));
#54041=CARTESIAN_POINT('',(-4.85,-2.4505,-3.00099698131059E-16));
#54042=CARTESIAN_POINT('Ctrl Pts',(-2.29167250378794,-2.45380537632986,
-0.00115034636150174));
#54043=CARTESIAN_POINT('Ctrl Pts',(-2.33048175492395,-2.44946767235673,
0.742949817427895));
#54044=CARTESIAN_POINT('Ctrl Pts',(-2.36929100605995,-2.08689533417843,
1.4907108692332));
#54045=CARTESIAN_POINT('Ctrl Pts',(-2.40810025719595,-1.49784486253987,
1.94446383384055));
#54046=CARTESIAN_POINT('Ctrl Pts',(-2.45034763012922,-0.856610254208518,
2.43841489329699));
#54047=CARTESIAN_POINT('Ctrl Pts',(-2.49259500306248,0.0530074563527559,
2.58395791301339));
#54048=CARTESIAN_POINT('Ctrl Pts',(-2.53484237599574,0.816351677303214,
2.31474593648947));
#54049=CARTESIAN_POINT('Ctrl Pts',(-2.577089748929,1.57969589825366,2.04553395996556));
#54050=CARTESIAN_POINT('Ctrl Pts',(-2.61933712186227,2.1967666295933,1.36156698720134));
#54051=CARTESIAN_POINT('Ctrl Pts',(-2.66158449479553,2.38626722282838,0.574636872262373));
#54052=CARTESIAN_POINT('Ctrl Pts',(-2.70383186772879,2.57576781606347,-0.212293242676599));
#54053=CARTESIAN_POINT('Ctrl Pts',(-2.74607924066205,2.337698271194,-1.10218649979031));
#54054=CARTESIAN_POINT('Ctrl Pts',(-2.78832661359532,1.78058449996468,-1.68937788796909));
#54055=CARTESIAN_POINT('Ctrl Pts',(-2.83057398652858,1.22347072873538,-2.27656927614787));
#54056=CARTESIAN_POINT('Ctrl Pts',(-2.87282135946184,0.347312731146226,
-2.56105879539171));
#54057=CARTESIAN_POINT('Ctrl Pts',(-2.9150687323951,-0.44848580650072,-2.41315960659802));
#54058=CARTESIAN_POINT('Ctrl Pts',(-2.95731610532836,-1.24428434414768,
-2.26526041780433));
#54059=CARTESIAN_POINT('Ctrl Pts',(-2.99956347826163,-1.95972342185244,
-1.6849725209731));
#54060=CARTESIAN_POINT('Ctrl Pts',(-3.04181085119489,-2.26866437439522,
-0.936824828835923));
#54061=CARTESIAN_POINT('Ctrl Pts',(-3.05843140205924,-2.39020492139988,
-0.642495834915862));
#54062=CARTESIAN_POINT('Ctrl Pts',(-3.07505195292359,-2.4488310831237,-0.322186903620115));
#54063=CARTESIAN_POINT('Ctrl Pts',(-3.09167250378794,-2.44725071792797,
-0.00132331670171071));
#54064=CARTESIAN_POINT('Ctrl Pts',(-3.20732749621206,-2.44741005262324,
-0.00144229910683621));
#54065=CARTESIAN_POINT('Ctrl Pts',(-3.19118827161173,-2.44908928680278,
-0.312962838534463));
#54066=CARTESIAN_POINT('Ctrl Pts',(-3.1750490470114,-2.3939145395726,-0.62391083234076));
#54067=CARTESIAN_POINT('Ctrl Pts',(-3.15890982241108,-2.27914261217474,
-0.911036188800726));
#54068=CARTESIAN_POINT('Ctrl Pts',(-3.11666244947782,-1.97870609560573,
-1.66263933661953));
#54069=CARTESIAN_POINT('Ctrl Pts',(-3.07441507654455,-1.26989396777807,
-2.25100348452715));
#54070=CARTESIAN_POINT('Ctrl Pts',(-3.03216770361129,-0.475823947375298,
-2.40791809562384));
#54071=CARTESIAN_POINT('Ctrl Pts',(-2.98992033067803,0.318246073027468,
-2.56483270672052));
#54072=CARTESIAN_POINT('Ctrl Pts',(-2.94767295774476,1.19757398600535,-2.29029778100629));
#54073=CARTESIAN_POINT('Ctrl Pts',(-2.9054255848115,1.76131107751761,-1.70946227601724));
#54074=CARTESIAN_POINT('Ctrl Pts',(-2.86317821187824,2.32504816902986,-1.1286267710282));
#54075=CARTESIAN_POINT('Ctrl Pts',(-2.82093083894498,2.57319443907647,-0.241490686764353));
#54076=CARTESIAN_POINT('Ctrl Pts',(-2.77868346601172,2.39263041244319,0.547537845298911));
#54077=CARTESIAN_POINT('Ctrl Pts',(-2.73643609307845,2.21206638580991,1.33656637736216));
#54078=CARTESIAN_POINT('Ctrl Pts',(-2.69418872014519,1.60279206249672,2.02748735722485));
#54079=CARTESIAN_POINT('Ctrl Pts',(-2.65194134721193,0.842550049158391,
2.30533889032187));
#54080=CARTESIAN_POINT('Ctrl Pts',(-2.60969397427867,0.0823080358200451,
2.58319042341891));
#54081=CARTESIAN_POINT('Ctrl Pts',(-2.5674466013454,-0.828901667543443,
2.44797250975027));
#54082=CARTESIAN_POINT('Ctrl Pts',(-2.52519922841214,-1.47569677223535,
1.96132532368679));
#54083=CARTESIAN_POINT('Ctrl Pts',(-2.48590865101211,-2.07722418940753,
1.50873744418155));
#54084=CARTESIAN_POINT('Ctrl Pts',(-2.44661807361209,-2.4500533600519,0.752190332549819));
#54085=CARTESIAN_POINT('Ctrl Pts',(-2.40732749621206,-2.45397025608505,
-0.00100410518415028));
#54086=CARTESIAN_POINT('Origin',(-4.85,0.,0.));
#54087=CARTESIAN_POINT('',(-1.49167250378794,-2.45055445589341,0.00221101876065513));
#54088=CARTESIAN_POINT('',(-1.60732749621206,-2.45027648577636,0.0022158123731987));
#54089=CARTESIAN_POINT('',(-4.85,-2.4505,-3.00099698131059E-16));
#54090=CARTESIAN_POINT('Ctrl Pts',(-1.49167250378794,-2.45055445589341,
0.00221101876065513));
#54091=CARTESIAN_POINT('Ctrl Pts',(-1.50141681105777,-2.45226598486262,
0.189685678637849));
#54092=CARTESIAN_POINT('Ctrl Pts',(-1.51116111832761,-2.43256006628774,
0.376804259058285));
#54093=CARTESIAN_POINT('Ctrl Pts',(-1.52090542559744,-2.39007174190195,
0.558598204251411));
#54094=CARTESIAN_POINT('Ctrl Pts',(-1.5631527985307,-2.20585956181267,1.34678318106949));
#54095=CARTESIAN_POINT('Ctrl Pts',(-1.60540017146397,-1.59339768921037,
2.03487893035977));
#54096=CARTESIAN_POINT('Ctrl Pts',(-1.64764754439723,-0.831879031878564,
2.30921131388054));
#54097=CARTESIAN_POINT('Ctrl Pts',(-1.68989491733049,-0.0703603745467456,
2.58354369740131));
#54098=CARTESIAN_POINT('Ctrl Pts',(-1.73214229026376,0.840215067514576,
2.44411271515255));
#54099=CARTESIAN_POINT('Ctrl Pts',(-1.77438966319702,1.48475269024887,1.95447918093393));
#54100=CARTESIAN_POINT('Ctrl Pts',(-1.81663703613028,2.12929031298315,1.46484564671533));
#54101=CARTESIAN_POINT('Ctrl Pts',(-1.85888440906354,2.5077901163904,0.625009560526885));
#54102=CARTESIAN_POINT('Ctrl Pts',(-1.9011317819968,2.44771067730732,-0.182183072094467));
#54103=CARTESIAN_POINT('Ctrl Pts',(-1.94337915493007,2.38763123822424,-0.989375704715836));
#54104=CARTESIAN_POINT('Ctrl Pts',(-1.98562652786333,1.8889725566508,-1.76392488377011));
#54105=CARTESIAN_POINT('Ctrl Pts',(-2.02787390079659,1.17905181075523,-2.15274610461772));
#54106=CARTESIAN_POINT('Ctrl Pts',(-2.07012127372986,0.469131064859669,
-2.54156732546532));
#54107=CARTESIAN_POINT('Ctrl Pts',(-2.11236864666312,-0.452051745358034,
-2.54466058810626));
#54108=CARTESIAN_POINT('Ctrl Pts',(-2.15461601959638,-1.16456780504994,
-2.16061581497033));
#54109=CARTESIAN_POINT('Ctrl Pts',(-2.19686339252964,-1.87708386474185,
-1.77657104183441));
#54110=CARTESIAN_POINT('Ctrl Pts',(-2.2391107654629,-2.38093317390796,-1.00538823292162));
#54111=CARTESIAN_POINT('Ctrl Pts',(-2.28135813839617,-2.4464320754403,-0.198617278866989));
#54112=CARTESIAN_POINT('Ctrl Pts',(-2.28479626019343,-2.45176242346953,
-0.13296167450759));
#54113=CARTESIAN_POINT('Ctrl Pts',(-2.28823438199068,-2.45418965466927,
-0.0670703761889925));
#54114=CARTESIAN_POINT('Ctrl Pts',(-2.29167250378794,-2.45380537632986,
-0.00115034636150174));
#54115=CARTESIAN_POINT('Ctrl Pts',(-2.40732749621206,-2.45397025608505,
-0.00100410518415028));
#54116=CARTESIAN_POINT('Ctrl Pts',(-2.40437070067883,-2.45426502041435,
-0.0576854292195473));
#54117=CARTESIAN_POINT('Ctrl Pts',(-2.40141390514559,-2.45247054215495,
-0.114347766223135));
#54118=CARTESIAN_POINT('Ctrl Pts',(-2.39845710961236,-2.44852706412429,
-0.170860144323412));
#54119=CARTESIAN_POINT('Ctrl Pts',(-2.35620973667909,-2.39218174530106,
-0.978321967811869));
#54120=CARTESIAN_POINT('Ctrl Pts',(-2.31396236374583,-1.89711060163426,
-1.75516915633047));
#54121=CARTESIAN_POINT('Ctrl Pts',(-2.27171499081257,-1.18899578697325,
-2.14726966381187));
#54122=CARTESIAN_POINT('Ctrl Pts',(-2.22946761787931,-0.480880972312235,
-2.53937017129327));
#54123=CARTESIAN_POINT('Ctrl Pts',(-2.18722024494604,0.440277513342999,
-2.54672399773748));
#54124=CARTESIAN_POINT('Ctrl Pts',(-2.14497287201278,1.15456212339647,-2.16597883548019));
#54125=CARTESIAN_POINT('Ctrl Pts',(-2.10272549907952,1.86884673344991,-1.78523367322291));
#54126=CARTESIAN_POINT('Ctrl Pts',(-2.06047812614626,2.37625746790161,-1.01638952226416));
#54127=CARTESIAN_POINT('Ctrl Pts',(-2.018230753213,2.44548711196819,-0.209930195652571));
#54128=CARTESIAN_POINT('Ctrl Pts',(-1.97598338027973,2.51471675603477,0.596529130959046));
#54129=CARTESIAN_POINT('Ctrl Pts',(-1.93373600734647,2.1457653097162,1.44060363322349));
#54130=CARTESIAN_POINT('Ctrl Pts',(-1.89148863441321,1.50682215458819,1.93751517313379));
#54131=CARTESIAN_POINT('Ctrl Pts',(-1.84924126147994,0.867878999460197,
2.43442671304407));
#54132=CARTESIAN_POINT('Ctrl Pts',(-1.80699388854668,-0.0410558644772366,
2.5841752906002));
#54133=CARTESIAN_POINT('Ctrl Pts',(-1.76474651561342,-0.805636951321461,
2.31849676426623));
#54134=CARTESIAN_POINT('Ctrl Pts',(-1.72249914268016,-1.57021803816568,
2.05281823793226));
#54135=CARTESIAN_POINT('Ctrl Pts',(-1.6802517697469,-2.1904453479167,1.37171260770819));
#54136=CARTESIAN_POINT('Ctrl Pts',(-1.63800439681363,-2.38358365619368,
0.585667450193285));
#54137=CARTESIAN_POINT('Ctrl Pts',(-1.62777876327978,-2.43033121526461,
0.395411603172733));
#54138=CARTESIAN_POINT('Ctrl Pts',(-1.61755312974592,-2.45205807642027,
0.199007950419292));
#54139=CARTESIAN_POINT('Ctrl Pts',(-1.60732749621206,-2.45027648577636,
0.0022158123731987));
#54140=CARTESIAN_POINT('Origin',(-4.85,0.,0.));
#54141=CARTESIAN_POINT('',(-0.691672503787938,-2.44670246171365,-0.000557269204686795));
#54142=CARTESIAN_POINT('',(-0.80732749621206,-2.44672029168306,-0.000703677119379069));
#54143=CARTESIAN_POINT('',(-4.85,-2.4505,-3.00099698131059E-16));
#54144=CARTESIAN_POINT('Ctrl Pts',(-0.691672503787938,-2.44670246171365,
-0.000557269204686795));
#54145=CARTESIAN_POINT('Ctrl Pts',(-0.714599240124866,-2.44575994471511,
0.442323777543362));
#54146=CARTESIAN_POINT('Ctrl Pts',(-0.737525976461795,-2.33087207722529,
0.88564371083638));
#54147=CARTESIAN_POINT('Ctrl Pts',(-0.760452712798723,-2.10494043458978,
1.26235300145016));
#54148=CARTESIAN_POINT('Ctrl Pts',(-0.802700085731985,-1.68861347799314,
1.956519744335));
#54149=CARTESIAN_POINT('Ctrl Pts',(-0.844947458665247,-0.895227651255518,
2.42450421239133));
#54150=CARTESIAN_POINT('Ctrl Pts',(-0.887194831598509,-0.0863207720182636,
2.45296481699518));
#54151=CARTESIAN_POINT('Ctrl Pts',(-0.929442204531771,0.722586107218991,
2.48142542159903));
#54152=CARTESIAN_POINT('Ctrl Pts',(-0.971689577465033,1.54701403895588,
2.07036216275039));
#54153=CARTESIAN_POINT('Ctrl Pts',(-1.0139369503983,2.01107092521102,1.4071652588015));
#54154=CARTESIAN_POINT('Ctrl Pts',(-1.05618432333156,2.47512781146617,0.743968354852607));
#54155=CARTESIAN_POINT('Ctrl Pts',(-1.09843169626482,2.57881365223958,-0.171362194196542));
#54156=CARTESIAN_POINT('Ctrl Pts',(-1.14067906919808,2.27489910948537,-0.921567533298358));
#54157=CARTESIAN_POINT('Ctrl Pts',(-1.18292644213135,1.97098456673116,-1.67177287240018));
#54158=CARTESIAN_POINT('Ctrl Pts',(-1.22517381506461,1.25946964044931,-2.25685300155467));
#54159=CARTESIAN_POINT('Ctrl Pts',(-1.26742118799787,0.46468490875651,-2.41009340789012));
#54160=CARTESIAN_POINT('Ctrl Pts',(-1.30966856093113,-0.330099822936278,
-2.56333381422556));
#54161=CARTESIAN_POINT('Ctrl Pts',(-1.3519159338644,-1.20815436004001,-2.28473449774198));
#54162=CARTESIAN_POINT('Ctrl Pts',(-1.39416330679766,-1.76920038480375,
-1.70129773732726));
#54163=CARTESIAN_POINT('Ctrl Pts',(-1.42666637246109,-2.20084179862391,
-1.25242998490692));
#54164=CARTESIAN_POINT('Ctrl Pts',(-1.45916943812451,-2.44484548788464,
-0.623128578142306));
#54165=CARTESIAN_POINT('Ctrl Pts',(-1.49167250378794,-2.45055445589341,
0.00221101876065513));
#54166=CARTESIAN_POINT('Ctrl Pts',(-1.60732749621206,-2.45027648577636,
0.0022158123731987));
#54167=CARTESIAN_POINT('Ctrl Pts',(-1.57530575681265,-2.44469740540674,
-0.614042000846752));
#54168=CARTESIAN_POINT('Ctrl Pts',(-1.54328401741325,-2.20858515756784,
-1.2341094543524));
#54169=CARTESIAN_POINT('Ctrl Pts',(-1.51126227801385,-1.78837913807019,
-1.68112422477864));
#54170=CARTESIAN_POINT('Ctrl Pts',(-1.46901490508058,-1.23398700486683,
-2.27088605742987));
#54171=CARTESIAN_POINT('Ctrl Pts',(-1.42676753214732,-0.359153431657199,
-2.55942503792661));
#54172=CARTESIAN_POINT('Ctrl Pts',(-1.38452015921406,0.437320224845424,
-2.41520802829028));
#54173=CARTESIAN_POINT('Ctrl Pts',(-1.3422727862808,1.23379388134807,-2.27099101865394));
#54174=CARTESIAN_POINT('Ctrl Pts',(-1.30002541334753,1.9519076211437,-1.69401801888449));
#54175=CARTESIAN_POINT('Ctrl Pts',(-1.25777804041427,2.2643062266558,-0.947307427860767));
#54176=CARTESIAN_POINT('Ctrl Pts',(-1.21553066748101,2.57670483216789,-0.200596836837063));
#54177=CARTESIAN_POINT('Ctrl Pts',(-1.17328329454775,2.48338830339646,0.715851345440913));
#54178=CARTESIAN_POINT('Ctrl Pts',(-1.13103592161449,2.02689055186718,1.38426799228393));
#54179=CARTESIAN_POINT('Ctrl Pts',(-1.08878854868123,1.57039280033789,2.05268463912697));
#54180=CARTESIAN_POINT('Ctrl Pts',(-1.04654117574796,0.75071382605072,2.47306975053505));
#54181=CARTESIAN_POINT('Ctrl Pts',(-1.0042938028147,-0.0584792284292852,
2.45378517339887));
#54182=CARTESIAN_POINT('Ctrl Pts',(-0.962046429881436,-0.867672282909301,
2.43450059626269));
#54183=CARTESIAN_POINT('Ctrl Pts',(-0.919799056948171,-1.66637941758216,
1.97554633058223));
#54184=CARTESIAN_POINT('Ctrl Pts',(-0.877551684014908,-2.09052238902825,
1.2861445967215));
#54185=CARTESIAN_POINT('Ctrl Pts',(-0.854143621413959,-2.32552789441308,
0.904166787854964));
#54186=CARTESIAN_POINT('Ctrl Pts',(-0.830735558813009,-2.44554401588084,
0.451442722424482));
#54187=CARTESIAN_POINT('Ctrl Pts',(-0.80732749621206,-2.44672029168306,
-0.000703677119379069));
#54188=CARTESIAN_POINT('Origin',(-4.85,0.,0.));
#54189=CARTESIAN_POINT('',(1.11022302462516E-15,-2.4505,-3.00099698131059E-16));
#54190=CARTESIAN_POINT('',(-0.00732749621205394,-2.45343455551405,-0.00158943503992818));
#54191=CARTESIAN_POINT('',(-4.85,-2.4505,-3.00099698131059E-16));
#54192=CARTESIAN_POINT('',(0.,-1.6158113816168,1.84230937386683));
#54193=CARTESIAN_POINT('Origin',(0.,0.,0.));
#54194=CARTESIAN_POINT('Ctrl Pts',(-1.73472347597681E-17,-1.6158113816168,
1.84230937386684));
#54195=CARTESIAN_POINT('Ctrl Pts',(-0.0422473729332622,-1.00451454043688,
2.37845189560396));
#54196=CARTESIAN_POINT('Ctrl Pts',(-0.0844947458665235,-0.110745570517432,
2.58195950654786));
#54197=CARTESIAN_POINT('Ctrl Pts',(-0.126742118799786,0.666815391991473,
2.36197006147115));
#54198=CARTESIAN_POINT('Ctrl Pts',(-0.168989491733048,1.44437635450039,
2.14198061639443));
#54199=CARTESIAN_POINT('Ctrl Pts',(-0.211236864666312,2.10572930959876,
1.49849411529711));
#54200=CARTESIAN_POINT('Ctrl Pts',(-0.253484237599575,2.34539034598602,
0.72516513771482));
#54201=CARTESIAN_POINT('Ctrl Pts',(-0.295731610532837,2.58505138237327,
-0.0481638398674565));
#54202=CARTESIAN_POINT('Ctrl Pts',(-0.337978983466098,2.40302050004942,
-0.951335293934691));
#54203=CARTESIAN_POINT('Ctrl Pts',(-0.38022635639936,1.88411977415752,-1.57274369054247));
#54204=CARTESIAN_POINT('Ctrl Pts',(-0.422473729332622,1.36521904826563,
-2.19415208715025));
#54205=CARTESIAN_POINT('Ctrl Pts',(-0.464721102265886,0.509448478805686,
-2.53379742629858));
#54206=CARTESIAN_POINT('Ctrl Pts',(-0.506968475199148,-0.294017051498195,
-2.43679826444183));
#54207=CARTESIAN_POINT('Ctrl Pts',(-0.54921584813241,-1.09748258180206,
-2.33979910258508));
#54208=CARTESIAN_POINT('Ctrl Pts',(-0.591463221065671,-1.84864307294988,
-1.80615543972326));
#54209=CARTESIAN_POINT('Ctrl Pts',(-0.633710593998932,-2.20458927529597,
-1.07915909943569));
#54210=CARTESIAN_POINT('Ctrl Pts',(-0.653031230595267,-2.36737116552707,
-0.746687962833883));
#54211=CARTESIAN_POINT('Ctrl Pts',(-0.672351867191602,-2.44749673212994,
-0.373778456637334));
#54212=CARTESIAN_POINT('Ctrl Pts',(-0.691672503787938,-2.44670246171365,
-0.000557269204686795));
#54213=CARTESIAN_POINT('Ctrl Pts',(-0.80732749621206,-2.44672029168306,
-0.000703677119379069));
#54214=CARTESIAN_POINT('Ctrl Pts',(-0.788488185879749,-2.44766698365207,
-0.364600787352598));
#54215=CARTESIAN_POINT('Ctrl Pts',(-0.769648875547439,-2.3716366477106,
-0.728123721712155));
#54216=CARTESIAN_POINT('Ctrl Pts',(-0.750809565215128,-2.21662198793308,
-1.05409038924796));
#54217=CARTESIAN_POINT('Ctrl Pts',(-0.708562192281865,-1.86899980717248,
-1.78507443931583));
#54218=CARTESIAN_POINT('Ctrl Pts',(-0.6663148193486,-1.12417663743191,-2.32719333741056));
#54219=CARTESIAN_POINT('Ctrl Pts',(-0.624067446415337,-0.321754636452474,
-2.43330246521825));
#54220=CARTESIAN_POINT('Ctrl Pts',(-0.581820073482074,0.48066736452695,
-2.53941159302594));
#54221=CARTESIAN_POINT('Ctrl Pts',(-0.539572700548812,1.34068819674525,
-2.20951095054658));
#54222=CARTESIAN_POINT('Ctrl Pts',(-0.49732532761555,1.86639110685498,-1.59401768292883));
#54223=CARTESIAN_POINT('Ctrl Pts',(-0.455077954682288,2.39209401696471,
-0.978524415311086));
#54224=CARTESIAN_POINT('Ctrl Pts',(-0.412830581749026,2.58347900496592,
-0.0774385225549623));
#54225=CARTESIAN_POINT('Ctrl Pts',(-0.370583208815764,2.35305240108692,
0.698528605099877));
#54226=CARTESIAN_POINT('Ctrl Pts',(-0.328335835882501,2.1226257972079,1.47449573275474));
#54227=CARTESIAN_POINT('Ctrl Pts',(-0.286088462949239,1.47038760144866,
2.12534409530829));
#54228=CARTESIAN_POINT('Ctrl Pts',(-0.243841090015977,0.694141965819649,
2.35427235402313));
#54229=CARTESIAN_POINT('Ctrl Pts',(-0.201593717082716,-0.0821036698093253,
2.58320061273796));
#54230=CARTESIAN_POINT('Ctrl Pts',(-0.159346344149453,-0.98235674530807,
2.39020876761409));
#54231=CARTESIAN_POINT('Ctrl Pts',(-0.117098971216192,-1.59714394385247,
1.86348026693122));
#54232=CARTESIAN_POINT('Ctrl Pts',(-0.0805084795481457,-2.12961174727059,
1.40728018921266));
#54233=CARTESIAN_POINT('Ctrl Pts',(-0.0439179878800999,-2.44794276668283,
0.700733923400609));
#54234=CARTESIAN_POINT('Ctrl Pts',(-0.00732749621205394,-2.45343455551405,
-0.00158943503992818));
#54235=CARTESIAN_POINT('Origin',(-11.2285451186048,0.,0.));
#54236=CARTESIAN_POINT('',(-0.428545118604763,-1.99165873719784,-0.000453626911316259));
#54237=CARTESIAN_POINT('',(-0.270454881395215,-1.99713877968237,-0.00129382801318301));
#54238=CARTESIAN_POINT('',(-11.2285451186048,-1.99475,-1.35786321299982E-13));
#54239=CARTESIAN_POINT('',(0.,1.94482913246214,0.443471766887781));
#54240=CARTESIAN_POINT('Ctrl Pts',(-0.428545118604763,-1.99165873719784,
-0.00045362691131607));
#54241=CARTESIAN_POINT('Ctrl Pts',(-0.409224482008429,-1.99230528725411,
-0.304262222557603));
#54242=CARTESIAN_POINT('Ctrl Pts',(-0.347656472478832,-1.78446077518961,
-1.27158386090278));
#54243=CARTESIAN_POINT('Ctrl Pts',(-0.243841090015977,-0.281912258858396,
-2.33903283263629));
#54244=CARTESIAN_POINT('Ctrl Pts',(-0.120313353744052,1.75492292348853,
-1.53063674963699));
#54245=CARTESIAN_POINT('Ctrl Pts',(-0.039032990405396,2.08014183670335,
-0.149753151782914));
#54246=CARTESIAN_POINT('Ctrl Pts',(-3.31223763694322E-16,1.94778769460277,
0.44492227130092));
#54247=CARTESIAN_POINT('',(0.,1.04832369103675,-1.69706953343435));
#54248=CARTESIAN_POINT('Origin',(0.,0.,0.));
#54249=CARTESIAN_POINT('Ctrl Pts',(-0.270454881395215,-1.99713877968237,
-0.00129382801318285));
#54250=CARTESIAN_POINT('Ctrl Pts',(-0.264798000130001,-1.99782990438245,
-0.0896790582877039));
#54251=CARTESIAN_POINT('Ctrl Pts',(-0.216893745931524,-1.95213957343271,
-0.837457295748683));
#54252=CARTESIAN_POINT('Ctrl Pts',(-0.126742118799788,-1.00466619559831,
-2.13028476617671));
#54253=CARTESIAN_POINT('Ctrl Pts',(-0.04224737293326,0.485218894542327,
-2.04491391286112));
#54254=CARTESIAN_POINT('Ctrl Pts',(2.22044604925031E-15,1.04832369103677,
-1.69706953343434));
#54255=CARTESIAN_POINT('Origin',(-11.2285451186048,0.,0.));
#54256=CARTESIAN_POINT('',(-1.22854511860476,-1.99479432805279,0.00179980806883705));
#54257=CARTESIAN_POINT('',(-1.07045488139522,-1.99167325110581,-0.000572805523073594));
#54258=CARTESIAN_POINT('',(-11.2285451186048,-1.99475,-1.35786321299982E-13));
#54259=CARTESIAN_POINT('Ctrl Pts',(-1.22854511860476,-1.99479432805279,
0.00179980806883711));
#54260=CARTESIAN_POINT('Ctrl Pts',(-1.19604205294134,-1.99014712791588,
-0.507237596918782));
#54261=CARTESIAN_POINT('Ctrl Pts',(-1.12129161434465,-1.53335398106482,
-1.68533687396134));
#54262=CARTESIAN_POINT('Ctrl Pts',(-1.0042938028147,0.446044752534434,-2.31338343704634));
#54263=CARTESIAN_POINT('Ctrl Pts',(-0.87755168401491,2.18360165830961,-0.884586961676926));
#54264=CARTESIAN_POINT('Ctrl Pts',(-0.750809565215123,1.93039537687792,
1.35069842422285));
#54265=CARTESIAN_POINT('Ctrl Pts',(-0.624067446415335,-0.0829010322208286,
2.35453654165394));
#54266=CARTESIAN_POINT('Ctrl Pts',(-0.516645964211884,-1.72503897850329,
1.38590939031426));
#54267=CARTESIAN_POINT('Ctrl Pts',(-0.451471854941692,-1.99089151182228,
0.360059316569889));
#54268=CARTESIAN_POINT('Ctrl Pts',(-0.428545118604763,-1.99165873719784,
-0.00045362691131607));
#54269=CARTESIAN_POINT('Ctrl Pts',(-1.07045488139522,-1.99167325110581,
-0.000572805523073629));
#54270=CARTESIAN_POINT('Ctrl Pts',(-1.05161557106291,-1.99244387498058,
-0.296791438715318));
#54271=CARTESIAN_POINT('Ctrl Pts',(-0.990528887797343,-1.79176473937272,
-1.25629618557132));
#54272=CARTESIAN_POINT('Ctrl Pts',(-0.887194831598507,-0.308800379382655,
-2.3356705087836));
#54273=CARTESIAN_POINT('Ctrl Pts',(-0.760452712798722,1.7914157663844,-1.5300357731145));
#54274=CARTESIAN_POINT('Ctrl Pts',(-0.633710593998933,2.25878798203272,
0.670463412246034));
#54275=CARTESIAN_POINT('Ctrl Pts',(-0.506968475199148,0.665987972658192,
2.25986937576817));
#54276=CARTESIAN_POINT('Ctrl Pts',(-0.385883237664576,-1.43435331803907,
1.80960849678481));
#54277=CARTESIAN_POINT('Ctrl Pts',(-0.307045373063264,-1.99266836720697,
0.570409709733958));
#54278=CARTESIAN_POINT('Ctrl Pts',(-0.270454881395215,-1.99713877968237,
-0.00129382801318285));
#54279=CARTESIAN_POINT('Origin',(-11.2285451186048,0.,0.));
#54280=CARTESIAN_POINT('',(-2.02854511860477,-1.9974406343334,-0.000936402123948542));
#54281=CARTESIAN_POINT('',(-1.87045488139522,-1.99456805549986,0.00180371015347854));
#54282=CARTESIAN_POINT('',(-11.2285451186048,-1.99475,-1.35786321299982E-13));
#54283=CARTESIAN_POINT('Ctrl Pts',(-2.02854511860477,-1.9974406343334,-0.000936402123948733));
#54284=CARTESIAN_POINT('Ctrl Pts',(-2.02510699680751,-1.99775344364478,
-0.0545964631312387));
#54285=CARTESIAN_POINT('Ctrl Pts',(-1.97942150207699,-1.97149905031364,
-0.767316398232434));
#54286=CARTESIAN_POINT('Ctrl Pts',(-1.89148863441321,-1.11783702498862,
-2.07391634106428));
#54287=CARTESIAN_POINT('Ctrl Pts',(-1.76474651561342,1.13173989076134,-2.06636243085856));
#54288=CARTESIAN_POINT('Ctrl Pts',(-1.63800439681363,2.34949064171247,-0.174872561543903));
#54289=CARTESIAN_POINT('Ctrl Pts',(-1.51126227801384,1.42517419668494,1.87605137184651));
#54290=CARTESIAN_POINT('Ctrl Pts',(-1.38452015921406,-0.798498967630685,
2.21654917046805));
#54291=CARTESIAN_POINT('Ctrl Pts',(-1.2902811060777,-1.91059945294607,0.967113652992006));
#54292=CARTESIAN_POINT('Ctrl Pts',(-1.2382894258746,-1.99618754266669,0.154407470909096));
#54293=CARTESIAN_POINT('Ctrl Pts',(-1.22854511860476,-1.99479432805279,
0.00179980806883711));
#54294=CARTESIAN_POINT('Ctrl Pts',(-1.87045488139522,-1.99456805549986,
0.0018037101534785));
#54295=CARTESIAN_POINT('Ctrl Pts',(-1.83843314199582,-1.99002658618038,
-0.49984096355409));
#54296=CARTESIAN_POINT('Ctrl Pts',(-1.76416402966316,-1.54425170067928,
-1.67051508410203));
#54297=CARTESIAN_POINT('Ctrl Pts',(-1.64764754439723,0.419772684089712,
-2.31829268547235));
#54298=CARTESIAN_POINT('Ctrl Pts',(-1.52090542559744,2.17344423984237,-0.909294246839299));
#54299=CARTESIAN_POINT('Ctrl Pts',(-1.39416330679766,1.94556036418415,1.3287204582401));
#54300=CARTESIAN_POINT('Ctrl Pts',(-1.26742118799787,-0.0561388408262527,
2.35532303034526));
#54301=CARTESIAN_POINT('Ctrl Pts',(-1.15951837953039,-1.71669807082336,
1.4011300490413));
#54302=CARTESIAN_POINT('Ctrl Pts',(-1.09386294399617,-1.9907157419622,0.367482297717186));
#54303=CARTESIAN_POINT('Ctrl Pts',(-1.07045488139522,-1.99167325110581,
-0.000572805523073629));
#54304=CARTESIAN_POINT('Origin',(-11.2285451186048,0.,0.));
#54305=CARTESIAN_POINT('',(-2.82854511860477,-1.99210502737679,-0.00107720301609401));
#54306=CARTESIAN_POINT('',(-2.67045488139522,-1.99757484934734,-0.000817359239539128));
#54307=CARTESIAN_POINT('',(-11.2285451186048,-1.99475,-1.35786321299982E-13));
#54308=CARTESIAN_POINT('Ctrl Pts',(-2.82854511860477,-1.99210502737679,
-0.00107720301609413));
#54309=CARTESIAN_POINT('Ctrl Pts',(-2.81192456774042,-1.99339147237746,
-0.262265793101971));
#54310=CARTESIAN_POINT('Ctrl Pts',(-2.7530566439428,-1.82436351865471,-1.18576413623229));
#54311=CARTESIAN_POINT('Ctrl Pts',(-2.65194134721193,-0.43048932676473,
-2.31632626019967));
#54312=CARTESIAN_POINT('Ctrl Pts',(-2.52519922841214,1.7091346263358,-1.62158787801847));
#54313=CARTESIAN_POINT('Ctrl Pts',(-2.39845710961236,2.29051298743969,0.551578301896968));
#54314=CARTESIAN_POINT('Ctrl Pts',(-2.27171499081256,0.783593777474662,
2.22186165499399));
#54315=CARTESIAN_POINT('Ctrl Pts',(-2.14841099381004,-1.37748262398157,
1.8760794855684));
#54316=CARTESIAN_POINT('Ctrl Pts',(-2.06735436974077,-1.99390966718369,
0.604774188253086));
#54317=CARTESIAN_POINT('Ctrl Pts',(-2.02854511860477,-1.9974406343334,-0.000936402123948733));
#54318=CARTESIAN_POINT('Ctrl Pts',(-2.67045488139522,-1.99757484934734,
-0.000817359239538885));
#54319=CARTESIAN_POINT('Ctrl Pts',(-2.66749808586199,-1.99781479268375,
-0.0469569516163979));
#54320=CARTESIAN_POINT('Ctrl Pts',(-2.62229391739549,-1.97548271348753,
-0.752113333853607));
#54321=CARTESIAN_POINT('Ctrl Pts',(-2.53484237599575,-1.14128472098778,
-2.06110573511026));
#54322=CARTESIAN_POINT('Ctrl Pts',(-2.40810025719595,1.1082327929001,-2.07906416640946));
#54323=CARTESIAN_POINT('Ctrl Pts',(-2.28135813839617,2.34735651770835,-0.201506276029945));
#54324=CARTESIAN_POINT('Ctrl Pts',(-2.15461601959638,1.44635766333907,1.8597680925381));
#54325=CARTESIAN_POINT('Ctrl Pts',(-2.02787390079659,-0.773309122834207,
2.22546200204237));
#54326=CARTESIAN_POINT('Ctrl Pts',(-1.93315352139621,-1.90526206476071,
0.982402385392531));
#54327=CARTESIAN_POINT('Ctrl Pts',(-1.88068051492908,-1.99601830154637,
0.161995963721133));
#54328=CARTESIAN_POINT('Ctrl Pts',(-1.87045488139522,-1.99456805549986,
0.0018037101534785));
#54329=CARTESIAN_POINT('Origin',(-11.2285451186048,0.,0.));
#54330=CARTESIAN_POINT('',(-3.62854511860477,-1.99356831942036,0.00170651223176268));
#54331=CARTESIAN_POINT('',(-3.47045488139522,-1.99223472861465,-0.00117405678175919));
#54332=CARTESIAN_POINT('',(-11.2285451186048,-1.99475,-1.35786321299982E-13));
#54333=CARTESIAN_POINT('Ctrl Pts',(-3.62854511860477,-1.99356831942036,
0.00170651223176254));
#54334=CARTESIAN_POINT('Ctrl Pts',(-3.59874213867332,-1.9897296575993,-0.465775611189874));
#54335=CARTESIAN_POINT('Ctrl Pts',(-3.52669178580862,-1.59272930081482,
-1.60181173444131));
#54336=CARTESIAN_POINT('Ctrl Pts',(-3.41239406001065,0.298056756295131,
-2.33706024159941));
#54337=CARTESIAN_POINT('Ctrl Pts',(-3.28565194121087,2.12296277169725,-1.02162491806891));
#54338=CARTESIAN_POINT('Ctrl Pts',(-3.15890982241107,2.0123294206081,1.22524230469704));
#54339=CARTESIAN_POINT('Ctrl Pts',(-3.03216770361129,0.067022912688436,
2.35503637594289));
#54340=CARTESIAN_POINT('Ctrl Pts',(-2.92204613567585,-1.67627504640892,
1.47111526782332));
#54341=CARTESIAN_POINT('Ctrl Pts',(-2.85417194067368,-1.99012148920151,
0.40164311469117));
#54342=CARTESIAN_POINT('Ctrl Pts',(-2.82854511860477,-1.99210502737679,
-0.00107720301609413));
#54343=CARTESIAN_POINT('Ctrl Pts',(-3.47045488139522,-1.99223472861465,
-0.00117405678175954));
#54344=CARTESIAN_POINT('Ctrl Pts',(-3.4543156567949,-1.99360165470304,-0.254757242263571));
#54345=CARTESIAN_POINT('Ctrl Pts',(-3.39592905926131,-1.83111989225785,
-1.17045474154989));
#54346=CARTESIAN_POINT('Ctrl Pts',(-3.29529508879446,-0.456730463269167,
-2.31129507643307));
#54347=CARTESIAN_POINT('Ctrl Pts',(-3.16855296999467,1.69063459008238,-1.64086633568406));
#54348=CARTESIAN_POINT('Ctrl Pts',(-3.04181085119489,2.29662084453102,0.525566682988035));
#54349=CARTESIAN_POINT('Ctrl Pts',(-2.9150687323951,0.808740873387587,2.21283208749455));
#54350=CARTESIAN_POINT('Ctrl Pts',(-2.79128340912855,-1.36456848198966,
1.8903263506637));
#54351=CARTESIAN_POINT('Ctrl Pts',(-2.70974545879525,-1.99438642724492,
0.612296129709636));
#54352=CARTESIAN_POINT('Ctrl Pts',(-2.67045488139522,-1.99757484934734,
-0.000817359239538885));
#54353=CARTESIAN_POINT('Origin',(-11.2285451186048,0.,0.));
#54354=CARTESIAN_POINT('',(-4.42854511860477,-1.99796240009219,-0.000212534135467141));
#54355=CARTESIAN_POINT('',(-4.27045488139522,-1.9933661524232,0.00166156985075161));
#54356=CARTESIAN_POINT('',(-11.2285451186048,-1.99475,-1.35786321299982E-13));
#54357=CARTESIAN_POINT('Ctrl Pts',(-4.42854511860477,-1.99796240009219,
-0.000212534135467313));
#54358=CARTESIAN_POINT('Ctrl Pts',(-4.42780708253949,-1.99797988321841,
-0.0117233257101024));
#54359=CARTESIAN_POINT('Ctrl Pts',(-4.38482167354096,-1.99268487938393,
-0.682129443554957));
#54360=CARTESIAN_POINT('Ctrl Pts',(-4.29958889160916,-1.24742757618837,
-1.9986527574939));
#54361=CARTESIAN_POINT('Ctrl Pts',(-4.17284677280937,0.998078354190639,
-2.13413401682469));
#54362=CARTESIAN_POINT('Ctrl Pts',(-4.04610465400959,2.33362016704573,-0.323890905768756));
#54363=CARTESIAN_POINT('Ctrl Pts',(-3.9193625352098,1.54156287203605,1.78164876292292));
#54364=CARTESIAN_POINT('Ctrl Pts',(-3.79262041641001,-0.655962132561314,
2.26283054679536));
#54365=CARTESIAN_POINT('Ctrl Pts',(-3.69568127754167,-1.87932505480736,
1.05292634598367));
#54366=CARTESIAN_POINT('Ctrl Pts',(-3.64098951160659,-1.99517117310856,
0.196906162688389));
#54367=CARTESIAN_POINT('Ctrl Pts',(-3.62854511860477,-1.99356831942036,
0.00170651223176254));
#54368=CARTESIAN_POINT('Ctrl Pts',(-4.27045488139522,-1.9933661524232,0.00166156985075149));
#54369=CARTESIAN_POINT('Ctrl Pts',(-4.24113322772781,-1.98971621390464,
-0.458388573709922));
#54370=CARTESIAN_POINT('Ctrl Pts',(-4.16956420112713,-1.60286571508947,
-1.58683223921642));
#54371=CARTESIAN_POINT('Ctrl Pts',(-4.05574780159318,0.271533578210096,
-2.34028997398879));
#54372=CARTESIAN_POINT('Ctrl Pts',(-3.9290056827934,2.11124012136177,-1.04563511631196));
#54373=CARTESIAN_POINT('Ctrl Pts',(-3.80226356399361,2.02609502746784,1.20234212520804));
#54374=CARTESIAN_POINT('Ctrl Pts',(-3.67552144519382,0.0937264506913446,
2.35412467784988));
#54375=CARTESIAN_POINT('Ctrl Pts',(-3.56491855099436,-1.66714663971742,
1.48625392461337));
#54376=CARTESIAN_POINT('Ctrl Pts',(-3.49656302972816,-1.99002347559849,
0.409043136748388));
#54377=CARTESIAN_POINT('Ctrl Pts',(-3.47045488139522,-1.99223472861465,
-0.00117405678175954));
#54378=CARTESIAN_POINT('Origin',(-11.2285451186048,0.,0.));
#54379=CARTESIAN_POINT('',(-5.22854511860477,-1.99297224531778,-0.00154381507001048));
#54380=CARTESIAN_POINT('',(-5.07045488139522,-1.99798725309096,-7.41124799008563E-5));
#54381=CARTESIAN_POINT('',(-11.2285451186048,-1.99475,-1.35786321299982E-13));
#54382=CARTESIAN_POINT('Ctrl Pts',(-5.22854511860477,-1.99297224531778,
-0.00154381507001065));
#54383=CARTESIAN_POINT('Ctrl Pts',(-5.2146246534724,-1.99456009233844,-0.220061877529497));
#54384=CARTESIAN_POINT('Ctrl Pts',(-5.15845681540677,-1.86083331804391,
-1.09987363392612));
#54385=CARTESIAN_POINT('Ctrl Pts',(-5.06004160440788,-0.576882037049555,
-2.28427133200172));
#54386=CARTESIAN_POINT('Ctrl Pts',(-4.93329948560809,1.60258234133143,-1.72696793314944));
#54387=CARTESIAN_POINT('Ctrl Pts',(-4.80655736680831,2.32094657675149,0.404839956945686));
#54388=CARTESIAN_POINT('Ctrl Pts',(-4.67981524800852,0.923266420793207,
2.16754873511761));
#54389=CARTESIAN_POINT('Ctrl Pts',(-4.55381116527401,-1.30313007054563,
1.95531152992337));
#54390=CARTESIAN_POINT('Ctrl Pts',(-4.47005445547276,-1.99697909722901,
0.647188517886537));
#54391=CARTESIAN_POINT('Ctrl Pts',(-4.42854511860477,-1.99796240009219,
-0.000212534135467313));
#54392=CARTESIAN_POINT('Ctrl Pts',(-5.07045488139522,-1.99798725309096,
-7.4112479900871E-5));
#54393=CARTESIAN_POINT('Ctrl Pts',(-5.07019817159397,-1.99798943639167,
-0.00407775576811743));
#54394=CARTESIAN_POINT('Ctrl Pts',(-5.02769408885946,-1.99616842066926,
-0.666968927304851));
#54395=CARTESIAN_POINT('Ctrl Pts',(-4.9429426331917,-1.27001347064424,-1.98437734084019));
#54396=CARTESIAN_POINT('Ctrl Pts',(-4.8162005143919,0.973811444563989,-2.14531557512957));
#54397=CARTESIAN_POINT('Ctrl Pts',(-4.68945839559212,2.3297967747643,-0.350335032157474));
#54398=CARTESIAN_POINT('Ctrl Pts',(-4.56271627679233,1.5616688454542,1.76405160457239));
#54399=CARTESIAN_POINT('Ctrl Pts',(-4.43597415799255,-0.630257733385777,
2.270123969294));
#54400=CARTESIAN_POINT('Ctrl Pts',(-4.33855369286017,-1.87340513851435,
1.06823330419032));
#54401=CARTESIAN_POINT('Ctrl Pts',(-4.28338060066107,-1.99497513673096,
0.204463194592811));
#54402=CARTESIAN_POINT('Ctrl Pts',(-4.27045488139522,-1.9933661524232,0.00166156985075149));
#54403=CARTESIAN_POINT('Origin',(-11.2285451186048,0.,0.));
#54404=CARTESIAN_POINT('',(-6.02854511860477,-1.99253871694387,0.00135657260398031));
#54405=CARTESIAN_POINT('',(-5.87045488139522,-1.99315854296458,-0.00160486565277951));
#54406=CARTESIAN_POINT('',(-11.2285451186048,-1.99475,-1.35786321299982E-13));
#54407=CARTESIAN_POINT('Ctrl Pts',(-6.02854511860477,-1.99253871694387,
0.00135657260398022));
#54408=CARTESIAN_POINT('Ctrl Pts',(-6.00144222440531,-1.98986087355467,
-0.424327265469242));
#54409=CARTESIAN_POINT('Ctrl Pts',(-5.93209195727259,-1.64787261177768,
-1.51748486420009));
#54410=CARTESIAN_POINT('Ctrl Pts',(-5.82049431720661,0.148871987083987,
-2.35128167908273));
#54411=CARTESIAN_POINT('Ctrl Pts',(-5.69375219840681,2.05371677028819,-1.15452840168687));
#54412=CARTESIAN_POINT('Ctrl Pts',(-5.56701007960703,2.08615488253003,1.09482702239254));
#54413=CARTESIAN_POINT('Ctrl Pts',(-5.44026796080724,0.216611974209998,
2.34601100924763));
#54414=CARTESIAN_POINT('Ctrl Pts',(-5.32744630713982,-1.62339131927296,
1.55579902148089));
#54415=CARTESIAN_POINT('Ctrl Pts',(-5.25687202640566,-1.98974111792884,
0.443120996720471));
#54416=CARTESIAN_POINT('Ctrl Pts',(-5.22854511860477,-1.99297224531778,
-0.00154381507001065));
#54417=CARTESIAN_POINT('Ctrl Pts',(-5.87045488139522,-1.99315854296458,
-0.00160486565277954));
#54418=CARTESIAN_POINT('Ctrl Pts',(-5.85701574252688,-1.99476242572242,
-0.212517444469958));
#54419=CARTESIAN_POINT('Ctrl Pts',(-5.80132923072528,-1.86697348923956,
-1.08456306234651));
#54420=CARTESIAN_POINT('Ctrl Pts',(-5.70339534599041,-0.60275022452326,
-2.27758201022554));
#54421=CARTESIAN_POINT('Ctrl Pts',(-5.57665322719063,1.58289408021768,-1.74503122529871));
#54422=CARTESIAN_POINT('Ctrl Pts',(-5.44991110839084,2.32538834689053,0.378492645374279));
#54423=CARTESIAN_POINT('Ctrl Pts',(-5.32316898959105,0.947788588779759,
2.15693867261862));
#54424=CARTESIAN_POINT('Ctrl Pts',(-5.19668358059252,-1.28938481843638,
1.96924988310733));
#54425=CARTESIAN_POINT('Ctrl Pts',(-5.11244554452723,-1.99763012514291,
0.654811816293906));
#54426=CARTESIAN_POINT('Ctrl Pts',(-5.07045488139522,-1.99798725309096,
-7.4112479900871E-5));
#54427=CARTESIAN_POINT('Origin',(-11.2285451186048,0.,0.));
#54428=CARTESIAN_POINT('',(-6.82854511860477,-1.99779957878814,0.000555587305033103));
#54429=CARTESIAN_POINT('',(-6.67045488139523,-1.99238576655478,0.0012713935872409));
#54430=CARTESIAN_POINT('',(-11.2285451186048,-1.99475,-1.35786321299982E-13));
#54431=CARTESIAN_POINT('Ctrl Pts',(-6.82854511860477,-1.99779957878814,
0.000555587305033239));
#54432=CARTESIAN_POINT('Ctrl Pts',(-6.78825979533822,-1.99546732181797,
-0.627892405283668));
#54433=CARTESIAN_POINT('Ctrl Pts',(-6.7057270991384,-1.33741286327219,-1.91960565321309));
#54434=CARTESIAN_POINT('Ctrl Pts',(-6.58094703000533,0.860378736396868,
-2.19327080752055));
#54435=CARTESIAN_POINT('Ctrl Pts',(-6.45420491120554,2.30830739273333,-0.471598752640533));
#54436=CARTESIAN_POINT('Ctrl Pts',(-6.32746279240575,1.65171500523044,1.68003748284402));
#54437=CARTESIAN_POINT('Ctrl Pts',(-6.20072067360598,-0.510772566486323,
2.29995647536138));
#54438=CARTESIAN_POINT('Ctrl Pts',(-6.10108144900563,-1.84473032498764,
1.13881147582941));
#54439=CARTESIAN_POINT('Ctrl Pts',(-6.04368959733857,-1.99403503471576,
0.239218986321839));
#54440=CARTESIAN_POINT('Ctrl Pts',(-6.02854511860477,-1.99253871694387,
0.00135657260398022));
#54441=CARTESIAN_POINT('Ctrl Pts',(-6.67045488139523,-1.99238576655478,
0.00127139358724077));
#54442=CARTESIAN_POINT('Ctrl Pts',(-6.64383331345979,-1.98993258053751,
-0.416933185350539));
#54443=CARTESIAN_POINT('Ctrl Pts',(-6.5749643725911,-1.65726775971581,-1.50238294145243));
#54444=CARTESIAN_POINT('Ctrl Pts',(-6.46384805878913,0.122197131302195,
-2.35281863047693));
#54445=CARTESIAN_POINT('Ctrl Pts',(-6.33710593998936,2.04049135411991,-1.17774474322024));
#54446=CARTESIAN_POINT('Ctrl Pts',(-6.21036382118955,2.09843673094916,1.07109800325793));
#54447=CARTESIAN_POINT('Ctrl Pts',(-6.08362170238978,0.243203528140627,
2.34340344166606));
#54448=CARTESIAN_POINT('Ctrl Pts',(-5.97031872245832,-1.61353055607485,
1.57082731498654));
#54449=CARTESIAN_POINT('Ctrl Pts',(-5.89926311546014,-1.98972044842943,
0.450508844706632));
#54450=CARTESIAN_POINT('Ctrl Pts',(-5.87045488139522,-1.99315854296458,
-0.00160486565277954));
#54451=CARTESIAN_POINT('Origin',(-11.2285451186048,0.,0.));
#54452=CARTESIAN_POINT('',(-7.62854511860478,-1.99410870701803,-0.00178313212496593));
#54453=CARTESIAN_POINT('',(-7.47045488139523,-1.99770021155217,0.000684642813972708));
#54454=CARTESIAN_POINT('',(-11.2285451186048,-1.99475,-1.35786321299982E-13));
#54455=CARTESIAN_POINT('Ctrl Pts',(-7.62854511860478,-1.99410870701803,
-0.00178313212496591));
#54456=CARTESIAN_POINT('Ctrl Pts',(-7.61732473920439,-1.99565114909841,
-0.1776621488792));
#54457=CARTESIAN_POINT('Ctrl Pts',(-7.56385698687075,-1.89390590255069,
-1.01401214084348));
#54458=CARTESIAN_POINT('Ctrl Pts',(-7.46814186160383,-0.720940648501152,
-2.24297408351883));
#54459=CARTESIAN_POINT('Ctrl Pts',(-7.34139974280405,1.48954593240367,-1.82536062259485));
#54460=CARTESIAN_POINT('Ctrl Pts',(-7.21465762400426,2.34198950274749,0.256463625198942));
#54461=CARTESIAN_POINT('Ctrl Pts',(-7.08791550520447,1.05920349809169,2.10446580356721));
#54462=CARTESIAN_POINT('Ctrl Pts',(-6.96117338640469,-1.18927539801392,
2.03379262579923));
#54463=CARTESIAN_POINT('Ctrl Pts',(-6.87471659087145,-1.98342949352272,
0.720717239997897));
#54464=CARTESIAN_POINT('Ctrl Pts',(-6.83050716827148,-1.99791316864271,
0.031163413541011));
#54465=CARTESIAN_POINT('Ctrl Pts',(-6.82854511860477,-1.99779957878814,
0.000555587305033239));
#54466=CARTESIAN_POINT('Ctrl Pts',(-7.47045488139522,-1.99770021155217,
0.000684642813972708));
#54467=CARTESIAN_POINT('Ctrl Pts',(-7.4306508843927,-1.99492802125712,-0.620336927842107));
#54468=CARTESIAN_POINT('Ctrl Pts',(-7.34859951445692,-1.35063127267045,
-1.90546653095491));
#54469=CARTESIAN_POINT('Ctrl Pts',(-7.22430077158785,0.835450035231239,
-2.20288694657198));
#54470=CARTESIAN_POINT('Ctrl Pts',(-7.09755865278807,2.30281051449999,-0.497746302890819));
#54471=CARTESIAN_POINT('Ctrl Pts',(-6.97081653398828,1.67066154010014,1.66119765838736));
#54472=CARTESIAN_POINT('Ctrl Pts',(-6.84407441518849,-0.484656478440782,
2.30560095130741));
#54473=CARTESIAN_POINT('Ctrl Pts',(-6.74395386432414,-1.83820373823975,
1.15412307625533));
#54474=CARTESIAN_POINT('Ctrl Pts',(-6.68608068639306,-1.99382568949329,
0.246740902202544));
#54475=CARTESIAN_POINT('Ctrl Pts',(-6.67045488139523,-1.99238576655478,
0.00127139358724077));
#54476=CARTESIAN_POINT('Origin',(-11.2285451186048,0.,0.));
#54477=CARTESIAN_POINT('',(-8.42854511860477,-1.99182883653917,0.000811954458581844));
#54478=CARTESIAN_POINT('',(-8.27045488139523,-1.99432920278645,-0.00179785228075047));
#54479=CARTESIAN_POINT('',(-11.2285451186048,-1.99475,-1.35786321299982E-13));
#54480=CARTESIAN_POINT('Ctrl Pts',(-8.42854511860477,-1.99182883653917,
0.000811954458581864));
#54481=CARTESIAN_POINT('Ctrl Pts',(-8.4041423101373,-1.99042079763708,-0.382807210105715));
#54482=CARTESIAN_POINT('Ctrl Pts',(-8.33749212873656,-1.69891434362089,
-1.43254947889824));
#54483=CARTESIAN_POINT('Ctrl Pts',(-8.22859457440256,-0.000914680687675627,
-2.35598723428903));
#54484=CARTESIAN_POINT('Ctrl Pts',(-8.10185245560277,1.97616110191247,-1.28276191309921));
#54485=CARTESIAN_POINT('Ctrl Pts',(-7.97511033680299,2.15153978631802,0.959982702237039));
#54486=CARTESIAN_POINT('Ctrl Pts',(-7.8483682180032,0.36532454981711,2.32749321407739));
#54487=CARTESIAN_POINT('Ctrl Pts',(-7.73284647860379,-1.56634391446507,
1.63978732290449));
#54488=CARTESIAN_POINT('Ctrl Pts',(-7.65957211213766,-1.98984349113318,
0.484563801492637));
#54489=CARTESIAN_POINT('Ctrl Pts',(-7.62854511860478,-1.99410870701803,
-0.00178313212496591));
#54490=CARTESIAN_POINT('Ctrl Pts',(-8.27045488139523,-1.99432920278645,
-0.00179785228075055));
#54491=CARTESIAN_POINT('Ctrl Pts',(-8.25971582825887,-1.99583155638226,
-0.170084723045423));
#54492=CARTESIAN_POINT('Ctrl Pts',(-8.20672940218925,-1.89945569290877,
-0.99871553949203));
#54493=CARTESIAN_POINT('Ctrl Pts',(-8.11149560318635,-0.746331107676049,
-2.23465339663279));
#54494=CARTESIAN_POINT('Ctrl Pts',(-7.98475348438659,1.4687490430934,-1.84213581757841));
#54495=CARTESIAN_POINT('Ctrl Pts',(-7.85801136558678,2.344747252036,0.229887303677403));
#54496=CARTESIAN_POINT('Ctrl Pts',(-7.73126924678701,1.08300149158113,2.09231813301428));
#54497=CARTESIAN_POINT('Ctrl Pts',(-7.60452712798722,-1.16613411679633,
2.04714898162071));
#54498=CARTESIAN_POINT('Ctrl Pts',(-7.51758900618996,-1.97963221169911,
0.735904795036756));
#54499=CARTESIAN_POINT('Ctrl Pts',(-7.47289825732596,-1.99787038298098,
0.0388061701096327));
#54500=CARTESIAN_POINT('Ctrl Pts',(-7.47045488139522,-1.99770021155217,
0.000684642813972708));
#54501=CARTESIAN_POINT('Origin',(-11.2285451186048,0.,0.));
#54502=CARTESIAN_POINT('',(-9.22854511860477,-1.99701091303081,0.00134739702958219));
#54503=CARTESIAN_POINT('',(-9.07045488139523,-1.99173797669883,0.000711821429190546));
#54504=CARTESIAN_POINT('',(-11.2285451186048,-1.99475,-1.35786321299982E-13));
#54505=CARTESIAN_POINT('Ctrl Pts',(-9.22854511860477,-1.99701091303081,
0.00134739702958217));
#54506=CARTESIAN_POINT('Ctrl Pts',(-9.1909598810702,-1.99279767918952,-0.585541655733389));
#54507=CARTESIAN_POINT('Ctrl Pts',(-9.11112727060237,-1.40970256146536,
-1.83984346058858));
#54508=CARTESIAN_POINT('Ctrl Pts',(-8.98904728720129,0.719219398296349,
-2.24341372601176));
#54509=CARTESIAN_POINT('Ctrl Pts',(-8.86230516840148,2.27364387353221,-0.617461289050906));
#54510=CARTESIAN_POINT('Ctrl Pts',(-8.73556304960172,1.75519010714565,1.57166161499472));
#54511=CARTESIAN_POINT('Ctrl Pts',(-8.60882093080191,-0.363519475821205,
2.32775941317825));
#54512=CARTESIAN_POINT('Ctrl Pts',(-8.5064816204696,-1.80667193342064,1.22468927408845));
#54513=CARTESIAN_POINT('Ctrl Pts',(-8.44638968307056,-1.99285846560797,
0.28133363791573));
#54514=CARTESIAN_POINT('Ctrl Pts',(-8.42854511860477,-1.99182883653917,
0.000811954458581864));
#54515=CARTESIAN_POINT('Ctrl Pts',(-9.07045488139523,-1.99173797669883,
0.000711821429190372));
#54516=CARTESIAN_POINT('Ctrl Pts',(-9.04653339919178,-1.99055413223079,
-0.375387133202429));
#54517=CARTESIAN_POINT('Ctrl Pts',(-8.98036454405507,-1.70760085155004,
-1.41737766741566));
#54518=CARTESIAN_POINT('Ctrl Pts',(-8.87194831598508,-0.0276278227480409,
-2.3558111213894));
#54519=CARTESIAN_POINT('Ctrl Pts',(-8.74520619718531,1.96148356546545,-1.30509783891208));
#54520=CARTESIAN_POINT('Ctrl Pts',(-8.61846407838551,2.16228968585577,0.935524719754586));
#54521=CARTESIAN_POINT('Ctrl Pts',(-8.49172195958573,0.391695740945932,
2.32319829923402));
#54522=CARTESIAN_POINT('Ctrl Pts',(-8.37571889392229,-1.55572672538957,
1.65467216178432));
#54523=CARTESIAN_POINT('Ctrl Pts',(-8.30196320119213,-1.98992130602461,
0.491954853320625));
#54524=CARTESIAN_POINT('Ctrl Pts',(-8.27045488139523,-1.99432920278645,
-0.00179785228075055));
#54525=CARTESIAN_POINT('Ctrl Pts',(-10.0126273851832,-0.875140871775484,
1.79252782880714));
#54526=CARTESIAN_POINT('Ctrl Pts',(-9.97038001224991,-1.46991969395398,
1.50214725641666));
#54527=CARTESIAN_POINT('Ctrl Pts',(-9.88588526638337,-2.33763048368433,
0.288012276356903));
#54528=CARTESIAN_POINT('Ctrl Pts',(-9.75914314758361,-1.51210248954419,
-1.80872878115075));
#54529=CARTESIAN_POINT('Ctrl Pts',(-9.63240102878379,0.693993151391669,
-2.25074530311671));
#54530=CARTESIAN_POINT('Ctrl Pts',(-9.50565890998404,2.2663578788523,-0.643561605617013));
#54531=CARTESIAN_POINT('Ctrl Pts',(-9.37891679118423,1.77297281393676,1.55184140168292));
#54532=CARTESIAN_POINT('Ctrl Pts',(-9.25217467238445,-0.337135258971208,
2.331634562323));
#54533=CARTESIAN_POINT('Ctrl Pts',(-9.12543255358466,-2.13972744825445,
0.986043024971392));
#54534=CARTESIAN_POINT('Ctrl Pts',(-8.99869043478488,-1.99157127464006,
-1.25875170116619));
#54535=CARTESIAN_POINT('Ctrl Pts',(-8.87194831598508,-0.0276278227480409,
-2.3558111213894));
#54536=CARTESIAN_POINT('Ctrl Pts',(-8.74520619718531,1.96148356546545,-1.30509783891208));
#54537=CARTESIAN_POINT('Ctrl Pts',(-8.61846407838551,2.16228968585577,0.935524719754586));
#54538=CARTESIAN_POINT('Ctrl Pts',(-8.49172195958573,0.391695740945932,
2.32319829923402));
#54539=CARTESIAN_POINT('Ctrl Pts',(-8.36497984078594,-1.73601052414358,
1.59278295504605));
#54540=CARTESIAN_POINT('Ctrl Pts',(-8.23823772198616,-2.28096959425052,
-0.589802678095906));
#54541=CARTESIAN_POINT('Ctrl Pts',(-8.11149560318635,-0.746331107676049,
-2.23465339663279));
#54542=CARTESIAN_POINT('Ctrl Pts',(-7.98475348438659,1.4687490430934,-1.84213581757841));
#54543=CARTESIAN_POINT('Ctrl Pts',(-7.85801136558678,2.344747252036,0.229887303677403));
#54544=CARTESIAN_POINT('Ctrl Pts',(-7.73126924678701,1.08300149158113,2.09231813301428));
#54545=CARTESIAN_POINT('Ctrl Pts',(-7.60452712798722,-1.16613411679633,
2.04714898162071));
#54546=CARTESIAN_POINT('Ctrl Pts',(-7.47778500918743,-2.35208649368352,
0.135561026464403));
#54547=CARTESIAN_POINT('Ctrl Pts',(-7.35104289038765,-1.39360369803105,
-1.89962005280031));
#54548=CARTESIAN_POINT('Ctrl Pts',(-7.22430077158785,0.835450035231239,
-2.20288694657198));
#54549=CARTESIAN_POINT('Ctrl Pts',(-7.09755865278807,2.30281051449999,-0.497746302890819));
#54550=CARTESIAN_POINT('Ctrl Pts',(-6.97081653398828,1.67066154010014,1.66119765838736));
#54551=CARTESIAN_POINT('Ctrl Pts',(-6.84407441518849,-0.484656478440782,
2.30560095130741));
#54552=CARTESIAN_POINT('Ctrl Pts',(-6.71733229638871,-2.19810537700899,
0.847950704926883));
#54553=CARTESIAN_POINT('Ctrl Pts',(-6.59059017758893,-1.90750618498507,
-1.38278986114584));
#54554=CARTESIAN_POINT('Ctrl Pts',(-6.46384805878913,0.122197131302195,
-2.35281863047693));
#54555=CARTESIAN_POINT('Ctrl Pts',(-6.33710593998936,2.04049135411991,-1.17774474322024));
#54556=CARTESIAN_POINT('Ctrl Pts',(-6.21036382118955,2.09843673094916,1.07109800325793));
#54557=CARTESIAN_POINT('Ctrl Pts',(-6.08362170238978,0.243203528140627,
2.34340344166606));
#54558=CARTESIAN_POINT('Ctrl Pts',(-5.95687958358998,-1.83376225002018,
1.47919020306685));
#54559=CARTESIAN_POINT('Ctrl Pts',(-5.8301374647902,-2.23885743746508,-0.733624577802266));
#54560=CARTESIAN_POINT('Ctrl Pts',(-5.70339534599041,-0.60275022452326,
-2.27758201022554));
#54561=CARTESIAN_POINT('Ctrl Pts',(-5.57665322719063,1.58289408021768,-1.74503122529871));
#54562=CARTESIAN_POINT('Ctrl Pts',(-5.44991110839084,2.32538834689053,0.378492645374279));
#54563=CARTESIAN_POINT('Ctrl Pts',(-5.32316898959105,0.947788588779759,
2.15693867261862));
#54564=CARTESIAN_POINT('Ctrl Pts',(-5.19642687079127,-1.29392529741552,
1.96886895733705));
#54565=CARTESIAN_POINT('Ctrl Pts',(-5.06968475199147,-2.35594664097114,
-0.0142503106843528));
#54566=CARTESIAN_POINT('Ctrl Pts',(-4.9429426331917,-1.27001347064424,-1.98437734084019));
#54567=CARTESIAN_POINT('Ctrl Pts',(-4.8162005143919,0.973811444563989,-2.14531557512957));
#54568=CARTESIAN_POINT('Ctrl Pts',(-4.68945839559212,2.3297967747643,-0.350335032157474));
#54569=CARTESIAN_POINT('Ctrl Pts',(-4.56271627679233,1.5616688454542,1.76405160457239));
#54570=CARTESIAN_POINT('Ctrl Pts',(-4.43597415799255,-0.630257733385777,
2.270123969294));
#54571=CARTESIAN_POINT('Ctrl Pts',(-4.30923203919275,-2.247568181374,0.706487732760443));
#54572=CARTESIAN_POINT('Ctrl Pts',(-4.18248992039297,-1.81573450338795,
-1.50126475335125));
#54573=CARTESIAN_POINT('Ctrl Pts',(-4.05574780159318,0.271533578210096,
-2.34028997398879));
#54574=CARTESIAN_POINT('Ctrl Pts',(-3.9290056827934,2.11124012136177,-1.04563511631196));
#54575=CARTESIAN_POINT('Ctrl Pts',(-3.80226356399361,2.02609502746784,1.20234212520804));
#54576=CARTESIAN_POINT('Ctrl Pts',(-3.67552144519382,0.0937264506913446,
2.35412467784988));
#54577=CARTESIAN_POINT('Ctrl Pts',(-3.54877932639404,-1.92409404154149,
1.35961382977754));
#54578=CARTESIAN_POINT('Ctrl Pts',(-3.42203720759425,-2.18768699293762,
-0.874478854390196));
#54579=CARTESIAN_POINT('Ctrl Pts',(-3.29529508879446,-0.456730463269167,
-2.31129507643307));
#54580=CARTESIAN_POINT('Ctrl Pts',(-3.16855296999467,1.69063459008238,-1.64086633568406));
#54581=CARTESIAN_POINT('Ctrl Pts',(-3.04181085119489,2.29662084453102,0.525566682988035));
#54582=CARTESIAN_POINT('Ctrl Pts',(-2.9150687323951,0.808740873387587,2.21283208749455));
#54583=CARTESIAN_POINT('Ctrl Pts',(-2.78832661359532,-1.41648119041691,
1.88262282413132));
#54584=CARTESIAN_POINT('Ctrl Pts',(-2.66158449479552,-2.35027451551463,
-0.164004005711231));
#54585=CARTESIAN_POINT('Ctrl Pts',(-2.53484237599575,-1.14128472098778,
-2.06110573511026));
#54586=CARTESIAN_POINT('Ctrl Pts',(-2.40810025719595,1.1082327929001,-2.07906416640946));
#54587=CARTESIAN_POINT('Ctrl Pts',(-2.28135813839617,2.34735651770835,-0.201506276029945));
#54588=CARTESIAN_POINT('Ctrl Pts',(-2.15461601959638,1.44635766333907,1.8597680925381));
#54589=CARTESIAN_POINT('Ctrl Pts',(-2.02787390079659,-0.773309122834207,
2.22546200204237));
#54590=CARTESIAN_POINT('Ctrl Pts',(-1.9011317819968,-2.28793686344939,0.562166198056052));
#54591=CARTESIAN_POINT('Ctrl Pts',(-1.77438966319702,-1.71661695495533,
-1.61366530573858));
#54592=CARTESIAN_POINT('Ctrl Pts',(-1.64764754439723,0.419772684089712,
-2.31829268547235));
#54593=CARTESIAN_POINT('Ctrl Pts',(-1.52090542559744,2.17344423984237,-0.909294246839299));
#54594=CARTESIAN_POINT('Ctrl Pts',(-1.39416330679766,1.94556036418415,1.3287204582401));
#54595=CARTESIAN_POINT('Ctrl Pts',(-1.26742118799787,-0.0561388408262527,
2.35532303034526));
#54596=CARTESIAN_POINT('Ctrl Pts',(-1.14067906919808,-2.00662370949219,
1.23453255313725));
#54597=CARTESIAN_POINT('Ctrl Pts',(-1.0139369503983,-2.12769776910723,-1.01178762124091));
#54598=CARTESIAN_POINT('Ctrl Pts',(-0.887194831598507,-0.308800379382655,
-2.3356705087836));
#54599=CARTESIAN_POINT('Ctrl Pts',(-0.760452712798722,1.7914157663844,-1.5300357731145));
#54600=CARTESIAN_POINT('Ctrl Pts',(-0.633710593998933,2.25878798203272,
0.670463412246034));
#54601=CARTESIAN_POINT('Ctrl Pts',(-0.506968475199148,0.665987972658192,
2.25986937576817));
#54602=CARTESIAN_POINT('Ctrl Pts',(-0.380226356399362,-1.53247742911832,
1.7885731304376));
#54603=CARTESIAN_POINT('Ctrl Pts',(-0.253484237599572,-2.33669743267895,
-0.312728077985436));
#54604=CARTESIAN_POINT('Ctrl Pts',(-0.126742118799788,-1.00466619559831,
-2.13028476617671));
#54605=CARTESIAN_POINT('Ctrl Pts',(-0.04224737293326,0.485218894542327,
-2.04491391286112));
#54606=CARTESIAN_POINT('Ctrl Pts',(2.22044604925031E-15,1.04832369103677,
-1.69706953343434));
#54607=CARTESIAN_POINT('Ctrl Pts',(-9.92491825678878,-0.941790067967425,
1.92904360906012));
#54608=CARTESIAN_POINT('Ctrl Pts',(-9.88267088385552,-1.58186620362845,
1.61654816080935));
#54609=CARTESIAN_POINT('Ctrl Pts',(-9.79817613798899,-2.51566032751424,
0.3099467869388));
#54610=CARTESIAN_POINT('Ctrl Pts',(-9.67143401918922,-1.62726156705764,
-1.94647839756206));
#54611=CARTESIAN_POINT('Ctrl Pts',(-9.54469190038941,0.746846454436609,
-2.42215812375346));
#54612=CARTESIAN_POINT('Ctrl Pts',(-9.41794978158964,2.43895972591532,-0.692574130454715));
#54613=CARTESIAN_POINT('Ctrl Pts',(-9.29120766278984,1.9079993185032,1.67002692515151));
#54614=CARTESIAN_POINT('Ctrl Pts',(-9.16446554399007,-0.362810889881688,
2.50920776728247));
#54615=CARTESIAN_POINT('Ctrl Pts',(-9.03772342519026,-2.30268534348643,
1.06113833493183));
#54616=CARTESIAN_POINT('Ctrl Pts',(-8.91098130639049,-2.14324585515011,
-1.35461602632079));
#54617=CARTESIAN_POINT('Ctrl Pts',(-8.78423918759069,-0.0297319093449403,
-2.53522557074784));
#54618=CARTESIAN_POINT('Ctrl Pts',(-8.65749706879091,2.11086671873626,-1.40449180475312));
#54619=CARTESIAN_POINT('Ctrl Pts',(-8.53075494999112,2.32696588159104,1.00677264406057));
#54620=CARTESIAN_POINT('Ctrl Pts',(-8.40401283119134,0.421526602613842,
2.50012901317076));
#54621=CARTESIAN_POINT('Ctrl Pts',(-8.27727071239154,-1.86822204545008,
1.71408651551934));
#54622=CARTESIAN_POINT('Ctrl Pts',(-8.15052859359177,-2.45468424396932,
-0.634721017159638));
#54623=CARTESIAN_POINT('Ctrl Pts',(-8.02378647479197,-0.803170377814069,
-2.40484068585289));
#54624=CARTESIAN_POINT('Ctrl Pts',(-7.89704435599219,1.58060639804846,-1.98242965537954));
#54625=CARTESIAN_POINT('Ctrl Pts',(-7.7703022371924,2.52331909648023,0.247395118132163));
#54626=CARTESIAN_POINT('Ctrl Pts',(-7.64356011839261,1.16548098855872,2.25166541782378));
#54627=CARTESIAN_POINT('Ctrl Pts',(-7.51681799959282,-1.25494484892315,
2.20305626296317));
#54628=CARTESIAN_POINT('Ctrl Pts',(-7.39007588079304,-2.53121728191868,
0.145885116836835));
#54629=CARTESIAN_POINT('Ctrl Pts',(-7.26333376199326,-1.49973811510549,
-2.04429178928587));
#54630=CARTESIAN_POINT('Ctrl Pts',(-7.13659164319346,0.899076446821093,
-2.37065495858689));
#54631=CARTESIAN_POINT('Ctrl Pts',(-7.00984952439368,2.47818853045577,-0.535653789633947));
#54632=CARTESIAN_POINT('Ctrl Pts',(-6.8831074055939,1.79789619722521,1.78771156285491));
#54633=CARTESIAN_POINT('Ctrl Pts',(-6.75636528679411,-0.521567067077507,
2.48119148204365));
#54634=CARTESIAN_POINT('Ctrl Pts',(-6.62962316799431,-2.36550923305976,
0.912529145628809));
#54635=CARTESIAN_POINT('Ctrl Pts',(-6.50288104919454,-2.05277851548714,
-1.48810071534096));
#54636=CARTESIAN_POINT('Ctrl Pts',(-6.37613893039474,0.131503450822755,
-2.53200517696812));
#54637=CARTESIAN_POINT('Ctrl Pts',(-6.24939681159496,2.19589160221116,-1.26743972032225));
#54638=CARTESIAN_POINT('Ctrl Pts',(-6.12265469279517,2.25824999746211,1.15267095141095));
#54639=CARTESIAN_POINT('Ctrl Pts',(-5.99591257399539,0.26172548293031,2.52187294386588));
#54640=CARTESIAN_POINT('Ctrl Pts',(-5.86917045519559,-1.97341837158038,
1.59184273848027));
#54641=CARTESIAN_POINT('Ctrl Pts',(-5.74242833639581,-2.40936489907259,
-0.789496140877558));
#54642=CARTESIAN_POINT('Ctrl Pts',(-5.61568621759603,-0.648654626048355,
-2.45103866747753));
#54643=CARTESIAN_POINT('Ctrl Pts',(-5.48894409879623,1.70344452130206,-1.87792974740757));
#54644=CARTESIAN_POINT('Ctrl Pts',(-5.36220197999645,2.50248585102143,0.407317982405529));
#54645=CARTESIAN_POINT('Ctrl Pts',(-5.23545986119667,1.01997050787345,2.32120734455678));
#54646=CARTESIAN_POINT('Ctrl Pts',(-5.10871774239687,-1.39246838206223,
2.11881456911904));
#54647=CARTESIAN_POINT('Ctrl Pts',(-4.98197562359709,-2.53537141126359,
-0.0153355893900096));
#54648=CARTESIAN_POINT('Ctrl Pts',(-4.8552335047973,-1.36673547243999,-2.1355040439505));
#54649=CARTESIAN_POINT('Ctrl Pts',(-4.72849138599752,1.04797521878131,-2.30869905231807));
#54650=CARTESIAN_POINT('Ctrl Pts',(-4.60174926719773,2.50723001704174,-0.377015934677563));
#54651=CARTESIAN_POINT('Ctrl Pts',(-4.47500714839794,1.68060280982999,1.89839868545702));
#54652=CARTESIAN_POINT('Ctrl Pts',(-4.34826502959816,-0.678257058612913,
2.44301263520966));
#54653=CARTESIAN_POINT('Ctrl Pts',(-4.22152291079836,-2.4187390379828,0.760292601241146));
#54654=CARTESIAN_POINT('Ctrl Pts',(-4.09478079199859,-1.954017663336,-1.61559844785595));
#54655=CARTESIAN_POINT('Ctrl Pts',(-3.96803867319879,0.292213099999658,
-2.51852235994282));
#54656=CARTESIAN_POINT('Ctrl Pts',(-3.84129655439901,2.27202847166641,-1.12526885558744));
#54657=CARTESIAN_POINT('Ctrl Pts',(-3.71455443559922,2.18039887653306,1.29391039584572));
#54658=CARTESIAN_POINT('Ctrl Pts',(-3.58781231679943,0.100864493036274,
2.53341069062175));
#54659=CARTESIAN_POINT('Ctrl Pts',(-3.46107019799964,-2.07062967414917,
1.46315963801102));
#54660=CARTESIAN_POINT('Ctrl Pts',(-3.33432807919986,-2.35429740310286,
-0.94107763249744));
#54661=CARTESIAN_POINT('Ctrl Pts',(-3.20758596040007,-0.491514255496263,
-2.48731926176697));
#54662=CARTESIAN_POINT('Ctrl Pts',(-3.08084384160029,1.819390359716,-1.76583184222006));
#54663=CARTESIAN_POINT('Ctrl Pts',(-2.9541017228005,2.47152746606171,0.56559292115852));
#54664=CARTESIAN_POINT('Ctrl Pts',(-2.82735960400071,0.870333161986235,
2.38135750402555));
#54665=CARTESIAN_POINT('Ctrl Pts',(-2.70061748520092,-1.52435791724691,
2.0260000814481));
#54666=CARTESIAN_POINT('Ctrl Pts',(-2.57387536640113,-2.5292673066657,-0.17649426357192));
#54667=CARTESIAN_POINT('Ctrl Pts',(-2.44713324760135,-1.22820296664768,
-2.21807593835652));
#54668=CARTESIAN_POINT('Ctrl Pts',(-2.32039112880156,1.19263386159946,-2.23740205233354));
#54669=CARTESIAN_POINT('Ctrl Pts',(-2.19364901000178,2.52612707925668,-0.216852641121762));
#54670=CARTESIAN_POINT('Ctrl Pts',(-2.06690689120199,1.55650973002526,2.00140477352138));
#54671=CARTESIAN_POINT('Ctrl Pts',(-1.9401647724022,-0.832202991361024,
2.39494929074703));
#54672=CARTESIAN_POINT('Ctrl Pts',(-1.81342265360242,-2.46218212818884,
0.604979791198736));
#54673=CARTESIAN_POINT('Ctrl Pts',(-1.68668053480263,-1.84735149599571,
-1.73655922947009));
#54674=CARTESIAN_POINT('Ctrl Pts',(-1.55993841600284,0.451741836577292,
-2.49484979645603));
#54675=CARTESIAN_POINT('Ctrl Pts',(-1.43319629720305,2.33896994687469,-0.978544504264554));
#54676=CARTESIAN_POINT('Ctrl Pts',(-1.30645417840327,2.09373083433111,1.4299134813997));
#54677=CARTESIAN_POINT('Ctrl Pts',(-1.17971205960348,-0.0604142766296505,
2.53470030754455));
#54678=CARTESIAN_POINT('Ctrl Pts',(-1.05296994080369,-2.15944465707978,
1.32855239039211));
#54679=CARTESIAN_POINT('Ctrl Pts',(-0.926227822003907,-2.2897395050425,
-1.08884359456764));
#54680=CARTESIAN_POINT('Ctrl Pts',(-0.799485703204116,-0.332318075485546,
-2.5135510843575));
#54681=CARTESIAN_POINT('Ctrl Pts',(-0.672743584404332,1.92784685391077,
-1.64656061809875));
#54682=CARTESIAN_POINT('Ctrl Pts',(-0.546001465604543,2.43081331901086,
0.721524731564423));
#54683=CARTESIAN_POINT('Ctrl Pts',(-0.419259346804758,0.716708450335271,
2.43197706979939));
#54684=CARTESIAN_POINT('Ctrl Pts',(-0.292517228004972,-1.64918822634783,
1.92478772778847));
#54685=CARTESIAN_POINT('Ctrl Pts',(-0.165775109205182,-2.51465621697831,
-0.336544900735453));
#54686=CARTESIAN_POINT('Ctrl Pts',(-0.0390329904053974,-1.08117981361961,
-2.29252352327827));
#54687=CARTESIAN_POINT('Ctrl Pts',(0.0454617554611303,0.522172315804407,
-2.20065097528105));
#54688=CARTESIAN_POINT('Ctrl Pts',(0.0877091283943924,1.12816218745486,
-1.82631537708437));
#54689=CARTESIAN_POINT('Ctrl Pts',(-9.83720912839439,-1.00843926415937,
2.0655593893131));
#54690=CARTESIAN_POINT('Ctrl Pts',(-9.79496175546113,-1.69381271330293,
1.73094906520204));
#54691=CARTESIAN_POINT('Ctrl Pts',(-9.7104670095946,-2.69369017134415,0.3318812975207));
#54692=CARTESIAN_POINT('Ctrl Pts',(-9.58372489079482,-1.74242064457108,
-2.08422801397338));
#54693=CARTESIAN_POINT('Ctrl Pts',(-9.45698277199502,0.799699757481549,
-2.5935709443902));
#54694=CARTESIAN_POINT('Ctrl Pts',(-9.33024065319525,2.61156157297835,-0.741586655292419));
#54695=CARTESIAN_POINT('Ctrl Pts',(-9.20349853439545,2.04302582306964,1.78821244862011));
#54696=CARTESIAN_POINT('Ctrl Pts',(-9.07675641559567,-0.38848652079217,
2.68678097224194));
#54697=CARTESIAN_POINT('Ctrl Pts',(-8.95001429679588,-2.4656432387184,1.13623364489228));
#54698=CARTESIAN_POINT('Ctrl Pts',(-8.8232721779961,-2.29492043566016,-1.45048035147539));
#54699=CARTESIAN_POINT('Ctrl Pts',(-8.6965300591963,-0.0318359959418395,
-2.71464002010627));
#54700=CARTESIAN_POINT('Ctrl Pts',(-8.56978794039653,2.26024987200707,-1.50388577059416));
#54701=CARTESIAN_POINT('Ctrl Pts',(-8.44304582159672,2.49164207732631,1.07802056836655));
#54702=CARTESIAN_POINT('Ctrl Pts',(-8.31630370279695,0.451357464281749,
2.67705972710749));
#54703=CARTESIAN_POINT('Ctrl Pts',(-8.18956158399716,-2.00043356675657,
1.83539007599263));
#54704=CARTESIAN_POINT('Ctrl Pts',(-8.06281946519737,-2.62839889368811,
-0.679639356223372));
#54705=CARTESIAN_POINT('Ctrl Pts',(-7.93607734639759,-0.860009647952086,
-2.57502797507298));
#54706=CARTESIAN_POINT('Ctrl Pts',(-7.80933522759779,1.69246375300351,-2.12272349318067));
#54707=CARTESIAN_POINT('Ctrl Pts',(-7.68259310879802,2.70189094092447,0.264902932586925));
#54708=CARTESIAN_POINT('Ctrl Pts',(-7.55585098999822,1.24796048553631,2.41101270263327));
#54709=CARTESIAN_POINT('Ctrl Pts',(-7.42910887119844,-1.34375558104996,
2.35896354430564));
#54710=CARTESIAN_POINT('Ctrl Pts',(-7.30236675239865,-2.71034807015384,
0.156209207209267));
#54711=CARTESIAN_POINT('Ctrl Pts',(-7.17562463359886,-1.60587253217993,
-2.18896352577142));
#54712=CARTESIAN_POINT('Ctrl Pts',(-7.04888251479907,0.962702858410947,
-2.53842297060179));
#54713=CARTESIAN_POINT('Ctrl Pts',(-6.92214039599929,2.65356654641154,-0.573561276377074));
#54714=CARTESIAN_POINT('Ctrl Pts',(-6.79539827719949,1.92513085435028,1.91422546732247));
#54715=CARTESIAN_POINT('Ctrl Pts',(-6.66865615839972,-0.558477655714234,
2.65678201277989));
#54716=CARTESIAN_POINT('Ctrl Pts',(-6.54191403959993,-2.53291308911053,
0.977107586330735));
#54717=CARTESIAN_POINT('Ctrl Pts',(-6.41517192080014,-2.1980508459892,-1.59341156953609));
#54718=CARTESIAN_POINT('Ctrl Pts',(-6.28842980200036,0.140809770343312,
-2.7111917234593));
#54719=CARTESIAN_POINT('Ctrl Pts',(-6.16168768320056,2.35129185030242,-1.35713469742426));
#54720=CARTESIAN_POINT('Ctrl Pts',(-6.03494556440078,2.41806326397505,1.23424389956398));
#54721=CARTESIAN_POINT('Ctrl Pts',(-5.90820344560099,0.280247437719996,
2.70034244606571));
#54722=CARTESIAN_POINT('Ctrl Pts',(-5.78146132680121,-2.11307449314059,
1.7044952738937));
#54723=CARTESIAN_POINT('Ctrl Pts',(-5.65471920800142,-2.5798723606801,-0.845367703952849));
#54724=CARTESIAN_POINT('Ctrl Pts',(-5.52797708920163,-0.694559027573452,
-2.62449532472953));
#54725=CARTESIAN_POINT('Ctrl Pts',(-5.40123497040184,1.82399496238643,-2.01082826951643));
#54726=CARTESIAN_POINT('Ctrl Pts',(-5.27449285160206,2.67958335515234,0.436143319436778));
#54727=CARTESIAN_POINT('Ctrl Pts',(-5.14775073280227,1.09215242696715,2.48547601649493));
#54728=CARTESIAN_POINT('Ctrl Pts',(-5.02100861400249,-1.49101146670894,
2.26876018090104));
#54729=CARTESIAN_POINT('Ctrl Pts',(-4.8942664952027,-2.71479618155604,-0.0164208680956645));
#54730=CARTESIAN_POINT('Ctrl Pts',(-4.76752437640291,-1.46345747423573,
-2.28663074706081));
#54731=CARTESIAN_POINT('Ctrl Pts',(-4.64078225760312,1.12213899299862,-2.47208252950658));
#54732=CARTESIAN_POINT('Ctrl Pts',(-4.51404013880334,2.68466325931919,-0.403696837197651));
#54733=CARTESIAN_POINT('Ctrl Pts',(-4.38729802000355,1.79953677420578,2.03274576634164));
#54734=CARTESIAN_POINT('Ctrl Pts',(-4.26055590120376,-0.726256383840051,
2.61590130112531));
#54735=CARTESIAN_POINT('Ctrl Pts',(-4.13381378240398,-2.58990989459159,
0.814097469721848));
#54736=CARTESIAN_POINT('Ctrl Pts',(-4.00707166360419,-2.09230082328405,
-1.72993214236066));
#54737=CARTESIAN_POINT('Ctrl Pts',(-3.8803295448044,0.312892621789216,-2.69675474589685));
#54738=CARTESIAN_POINT('Ctrl Pts',(-3.75358742600461,2.43281682197106,-1.20490259486291));
#54739=CARTESIAN_POINT('Ctrl Pts',(-3.62684530720483,2.33470272559827,1.38547866648339));
#54740=CARTESIAN_POINT('Ctrl Pts',(-3.50010318840504,0.108002535381206,
2.71269670339363));
#54741=CARTESIAN_POINT('Ctrl Pts',(-3.37336106960526,-2.21716530675685,
1.56670544624449));
#54742=CARTESIAN_POINT('Ctrl Pts',(-3.24661895080546,-2.52090781326811,
-1.00767641060468));
#54743=CARTESIAN_POINT('Ctrl Pts',(-3.11987683200569,-0.526298047723356,
-2.66334344710087));
#54744=CARTESIAN_POINT('Ctrl Pts',(-2.99313471320588,1.94814612934961,-1.89079734875606));
#54745=CARTESIAN_POINT('Ctrl Pts',(-2.86639259440611,2.6464340875924,0.605619159329004));
#54746=CARTESIAN_POINT('Ctrl Pts',(-2.73965047560631,0.931925450584883,
2.54988292055654));
#54747=CARTESIAN_POINT('Ctrl Pts',(-2.61290835680654,-1.63223464407691,
2.16937733876486));
#54748=CARTESIAN_POINT('Ctrl Pts',(-2.48616623800674,-2.70826009781677,
-0.188984521432605));
#54749=CARTESIAN_POINT('Ctrl Pts',(-2.35942411920696,-1.31512121230757,
-2.37504614160279));
#54750=CARTESIAN_POINT('Ctrl Pts',(-2.23268200040717,1.27703493029882,-2.39573993825761));
#54751=CARTESIAN_POINT('Ctrl Pts',(-2.10593988160739,2.704897640805,-0.232199006213583));
#54752=CARTESIAN_POINT('Ctrl Pts',(-1.97919776280759,1.66666179671145,2.14304145450466));
#54753=CARTESIAN_POINT('Ctrl Pts',(-1.85245564400781,-0.891096859887847,
2.56443657945168));
#54754=CARTESIAN_POINT('Ctrl Pts',(-1.72571352520802,-2.63642739292829,
0.647793384341421));
#54755=CARTESIAN_POINT('Ctrl Pts',(-1.59897140640824,-1.97808603703611,
-1.8594531532016));
#54756=CARTESIAN_POINT('Ctrl Pts',(-1.47222928760845,0.48371098906488,-2.6714069074397));
#54757=CARTESIAN_POINT('Ctrl Pts',(-1.34548716880866,2.504495653907,-1.04779476168981));
#54758=CARTESIAN_POINT('Ctrl Pts',(-1.21874505000888,2.24190130447808,1.53110650455931));
#54759=CARTESIAN_POINT('Ctrl Pts',(-1.09200293120909,-0.0646897124330518,
2.71407758474384));
#54760=CARTESIAN_POINT('Ctrl Pts',(-0.965260812409299,-2.31226560466736,
1.42257222764696));
#54761=CARTESIAN_POINT('Ctrl Pts',(-0.838518693609519,-2.45178124097777,
-1.16589956789437));
#54762=CARTESIAN_POINT('Ctrl Pts',(-0.711776574809725,-0.355835771588435,
-2.6914316599314));
#54763=CARTESIAN_POINT('Ctrl Pts',(-0.585034456009942,2.06427794143713,
-1.763085463083));
#54764=CARTESIAN_POINT('Ctrl Pts',(-0.458292337210153,2.602838655989,0.77258605088281));
#54765=CARTESIAN_POINT('Ctrl Pts',(-0.331550218410368,0.767428928012345,
2.60408476383061));
#54766=CARTESIAN_POINT('Ctrl Pts',(-0.204808099610581,-1.76589902357732,
2.06100232513935));
#54767=CARTESIAN_POINT('Ctrl Pts',(-0.0780659808107919,-2.69261500127767,
-0.360361723485471));
#54768=CARTESIAN_POINT('Ctrl Pts',(0.048676137988993,-1.15769343164092,
-2.45476228037983));
#54769=CARTESIAN_POINT('Ctrl Pts',(0.13317088385552,0.559125737066487,-2.35638803770098));
#54770=CARTESIAN_POINT('Ctrl Pts',(0.175418256788783,1.20800068387295,-1.95556122073441));
#54771=CARTESIAN_POINT('Ctrl Pts',(-9.7495,-1.07508846035131,2.20207516956608));
#54772=CARTESIAN_POINT('Ctrl Pts',(-9.70725262706674,-1.80575922297741,
1.84534996959472));
#54773=CARTESIAN_POINT('Ctrl Pts',(-9.62275788120021,-2.87172001517406,
0.353815808102598));
#54774=CARTESIAN_POINT('Ctrl Pts',(-9.49601576240043,-1.85757972208452,
-2.22197763038469));
#54775=CARTESIAN_POINT('Ctrl Pts',(-9.36927364360064,0.852553060526489,
-2.76498376502695));
#54776=CARTESIAN_POINT('Ctrl Pts',(-9.24253152480086,2.78416342004137,-0.790599180130123));
#54777=CARTESIAN_POINT('Ctrl Pts',(-9.11578940600106,2.17805232763608,1.9063979720887));
#54778=CARTESIAN_POINT('Ctrl Pts',(-8.98904728720128,-0.414162151702653,
2.86435417720141));
#54779=CARTESIAN_POINT('Ctrl Pts',(-8.86230516840148,-2.62860113395038,
1.21132895485272));
#54780=CARTESIAN_POINT('Ctrl Pts',(-8.73556304960171,-2.44659501617021,
-1.54634467663));
#54781=CARTESIAN_POINT('Ctrl Pts',(-8.6088209308019,-0.0339400825387369,
-2.89405446946471));
#54782=CARTESIAN_POINT('Ctrl Pts',(-8.48207881200215,2.40963302527788,-1.60327973643519));
#54783=CARTESIAN_POINT('Ctrl Pts',(-8.35533669320233,2.65631827306158,1.14926849267254));
#54784=CARTESIAN_POINT('Ctrl Pts',(-8.22859457440257,0.481188325949657,
2.85399044104422));
#54785=CARTESIAN_POINT('Ctrl Pts',(-8.10185245560276,-2.13264508806306,
1.95669363646592));
#54786=CARTESIAN_POINT('Ctrl Pts',(-7.97511033680299,-2.80211354340691,
-0.724557695287102));
#54787=CARTESIAN_POINT('Ctrl Pts',(-7.8483682180032,-0.9168489180901,-2.74521526429308));
#54788=CARTESIAN_POINT('Ctrl Pts',(-7.7216260992034,1.80432110795856,-2.2630173309818));
#54789=CARTESIAN_POINT('Ctrl Pts',(-7.59488398040362,2.8804627853687,0.282410747041685));
#54790=CARTESIAN_POINT('Ctrl Pts',(-7.46814186160384,1.33043998251391,2.57035998744277));
#54791=CARTESIAN_POINT('Ctrl Pts',(-7.34139974280405,-1.43256631317677,
2.51487082564811));
#54792=CARTESIAN_POINT('Ctrl Pts',(-7.21465762400426,-2.889478858389,0.166533297581697));
#54793=CARTESIAN_POINT('Ctrl Pts',(-7.08791550520448,-1.71200694925436,
-2.33363526225698));
#54794=CARTESIAN_POINT('Ctrl Pts',(-6.96117338640468,1.02632927000079,-2.7061909826167));
#54795=CARTESIAN_POINT('Ctrl Pts',(-6.8344312676049,2.82894456236732,-0.611468763120201));
#54796=CARTESIAN_POINT('Ctrl Pts',(-6.70768914880512,2.05236551147535,2.04073937179003));
#54797=CARTESIAN_POINT('Ctrl Pts',(-6.58094703000532,-0.595388244350957,
2.83237254351614));
#54798=CARTESIAN_POINT('Ctrl Pts',(-6.45420491120554,-2.7003169451613,1.04168602703266));
#54799=CARTESIAN_POINT('Ctrl Pts',(-6.32746279240576,-2.34332317649127,
-1.69872242373121));
#54800=CARTESIAN_POINT('Ctrl Pts',(-6.20072067360596,0.150116089863871,
-2.89037826995048));
#54801=CARTESIAN_POINT('Ctrl Pts',(-6.07397855480618,2.50669209839368,-1.44682967452627));
#54802=CARTESIAN_POINT('Ctrl Pts',(-5.94723643600639,2.577876530488,1.315816847717));
#54803=CARTESIAN_POINT('Ctrl Pts',(-5.8204943172066,0.298769392509677,2.87881194826553));
#54804=CARTESIAN_POINT('Ctrl Pts',(-5.69375219840682,-2.25273061470079,
1.81714780930712));
#54805=CARTESIAN_POINT('Ctrl Pts',(-5.56701007960703,-2.75037982228761,
-0.901239267028141));
#54806=CARTESIAN_POINT('Ctrl Pts',(-5.44026796080724,-0.740463429098543,
-2.79795198198153));
#54807=CARTESIAN_POINT('Ctrl Pts',(-5.31352584200746,1.9445454034708,-2.14372679162529));
#54808=CARTESIAN_POINT('Ctrl Pts',(-5.18678372320766,2.85668085928325,0.464968656468029));
#54809=CARTESIAN_POINT('Ctrl Pts',(-5.06004160440788,1.16433434606084,2.64974468843308));
#54810=CARTESIAN_POINT('Ctrl Pts',(-4.9332994856081,-1.58955455135565,2.41870579268303));
#54811=CARTESIAN_POINT('Ctrl Pts',(-4.8065573668083,-2.89422095184849,-0.0175061468013224));
#54812=CARTESIAN_POINT('Ctrl Pts',(-4.67981524800852,-1.56017947603147,
-2.43775745017111));
#54813=CARTESIAN_POINT('Ctrl Pts',(-4.55307312920873,1.19630276721594,-2.63546600669509));
#54814=CARTESIAN_POINT('Ctrl Pts',(-4.42633101040895,2.86209650159664,-0.430377739717738));
#54815=CARTESIAN_POINT('Ctrl Pts',(-4.29958889160916,1.91847073858157,2.16709284722627));
#54816=CARTESIAN_POINT('Ctrl Pts',(-4.17284677280938,-0.774255709067188,
2.78878996704097));
#54817=CARTESIAN_POINT('Ctrl Pts',(-4.04610465400958,-2.76108075120038,
0.86790233820255));
#54818=CARTESIAN_POINT('Ctrl Pts',(-3.9193625352098,-2.2305839832321,-1.84426583686536));
#54819=CARTESIAN_POINT('Ctrl Pts',(-3.79262041641001,0.333572143578779,
-2.87498713185087));
#54820=CARTESIAN_POINT('Ctrl Pts',(-3.66587829761023,2.59360517227571,-1.28453633413838));
#54821=CARTESIAN_POINT('Ctrl Pts',(-3.53913617881044,2.48900657466348,1.47704693712107));
#54822=CARTESIAN_POINT('Ctrl Pts',(-3.41239406001065,0.115140577726135,
2.8919827161655));
#54823=CARTESIAN_POINT('Ctrl Pts',(-3.28565194121086,-2.36370093936452,
1.67025125447797));
#54824=CARTESIAN_POINT('Ctrl Pts',(-3.15890982241108,-2.68751822343335,
-1.07427518871192));
#54825=CARTESIAN_POINT('Ctrl Pts',(-3.03216770361129,-0.561081839950451,
-2.83936763243476));
#54826=CARTESIAN_POINT('Ctrl Pts',(-2.9054255848115,2.07690189898324,-2.01576285529206));
#54827=CARTESIAN_POINT('Ctrl Pts',(-2.77868346601172,2.82134070912309,0.645645397499492));
#54828=CARTESIAN_POINT('Ctrl Pts',(-2.65194134721193,0.993517739183532,
2.71840833708754));
#54829=CARTESIAN_POINT('Ctrl Pts',(-2.52519922841214,-1.74011137090692,
2.31275459608164));
#54830=CARTESIAN_POINT('Ctrl Pts',(-2.39845710961236,-2.88725288896784,
-0.201474779293297));
#54831=CARTESIAN_POINT('Ctrl Pts',(-2.27171499081257,-1.40203945796747,
-2.53201634484905));
#54832=CARTESIAN_POINT('Ctrl Pts',(-2.14497287201278,1.36143599899819,-2.55407782418169));
#54833=CARTESIAN_POINT('Ctrl Pts',(-2.01823075321299,2.88366820235333,-0.2475453713054));
#54834=CARTESIAN_POINT('Ctrl Pts',(-1.89148863441321,1.77681386339764,2.28467813548794));
#54835=CARTESIAN_POINT('Ctrl Pts',(-1.76474651561342,-0.949990728414667,
2.73392386815634));
#54836=CARTESIAN_POINT('Ctrl Pts',(-1.63800439681363,-2.81067265766773,
0.690606977484108));
#54837=CARTESIAN_POINT('Ctrl Pts',(-1.51126227801385,-2.10882057807649,
-1.98234707693312));
#54838=CARTESIAN_POINT('Ctrl Pts',(-1.38452015921406,0.515680141552461,
-2.84796401842337));
#54839=CARTESIAN_POINT('Ctrl Pts',(-1.25777804041427,2.67002136093931,-1.11704501911506));
#54840=CARTESIAN_POINT('Ctrl Pts',(-1.13103592161449,2.39007177462504,1.63229952771891));
#54841=CARTESIAN_POINT('Ctrl Pts',(-1.0042938028147,-0.0689651482364484,
2.89345486194313));
#54842=CARTESIAN_POINT('Ctrl Pts',(-0.87755168401491,-2.46508655225495,
1.51659206490182));
#54843=CARTESIAN_POINT('Ctrl Pts',(-0.750809565215129,-2.61382297691304,
-1.2429555412211));
#54844=CARTESIAN_POINT('Ctrl Pts',(-0.624067446415335,-0.379353467691326,
-2.8693122355053));
#54845=CARTESIAN_POINT('Ctrl Pts',(-0.497325327615552,2.2007090289635,-1.87961030806724));
#54846=CARTESIAN_POINT('Ctrl Pts',(-0.370583208815762,2.77486399296714,
0.823647370201196));
#54847=CARTESIAN_POINT('Ctrl Pts',(-0.243841090015978,0.818149405689422,
2.77619245786183));
#54848=CARTESIAN_POINT('Ctrl Pts',(-0.117098971216191,-1.88260982080682,
2.19721692249022));
#54849=CARTESIAN_POINT('Ctrl Pts',(0.00964314758359831,-2.87057378557703,
-0.384178546235488));
#54850=CARTESIAN_POINT('Ctrl Pts',(0.136385266383383,-1.23420704966222,
-2.61700103748139));
#54851=CARTESIAN_POINT('Ctrl Pts',(0.220880012249911,0.596079158328567,
-2.51212510012091));
#54852=CARTESIAN_POINT('Ctrl Pts',(0.263127385183173,1.28783918029104,-2.08480706438444));
#54853=CARTESIAN_POINT('',(0.,-2.44644308591689,-0.140948491901913));
#54854=CARTESIAN_POINT('Ctrl Pts',(7.21644966006352E-16,-2.45032305592699,
-0.14210232202442));
#54855=CARTESIAN_POINT('Ctrl Pts',(8.8338875589462E-16,-2.44155110065596,
-0.203186250076526));
#54856=CARTESIAN_POINT('Ctrl Pts',(3.38686818731122E-15,-2.43033064707317,
-0.263814673487791));
#54857=CARTESIAN_POINT('Ctrl Pts',(3.33066907387547E-15,-2.41660092933931,
-0.32386049272943));
#54858=CARTESIAN_POINT('Ctrl Pts',(3.19830583638964E-15,-2.39759379521507,
-0.406986669250303));
#54859=CARTESIAN_POINT('Ctrl Pts',(3.59208164640204E-15,-2.37377911238307,
-0.488997644336173));
#54860=CARTESIAN_POINT('Ctrl Pts',(3.49720252756924E-15,-2.34542524376074,
-0.569597439065157));
#54861=CARTESIAN_POINT('Ctrl Pts',(3.4494265021795E-15,-2.33114775927456,
-0.610183164214713));
#54862=CARTESIAN_POINT('Ctrl Pts',(7.57069741264941E-15,-2.31571859533792,
-0.650410667591147));
#54863=CARTESIAN_POINT('Ctrl Pts',(7.35522753814166E-15,-2.29916808587573,
-0.690239206674431));
#54864=CARTESIAN_POINT('Ctrl Pts',(7.25579217878261E-15,-2.29153033206116,
-0.708619340349916));
#54865=CARTESIAN_POINT('Ctrl Pts',(7.532000478547E-15,-2.28365373778081,
-0.726914477167649));
#54866=CARTESIAN_POINT('Ctrl Pts',(7.66053886991358E-15,-2.27554112542911,
-0.745120441436594));
#54867=CARTESIAN_POINT('Ctrl Pts',(7.75996668184755E-15,-2.26926580731891,
-0.759203231583288));
#54868=CARTESIAN_POINT('Ctrl Pts',(3.19768457339427E-15,-2.26285104588459,
-0.773228550540596));
#54869=CARTESIAN_POINT('Ctrl Pts',(3.41393580072236E-15,-2.25630175870705,
-0.787187609752352));
#54870=CARTESIAN_POINT('Ctrl Pts',(4.60505114880462E-15,-2.22022817626985,
-0.864074339494172));
#54871=CARTESIAN_POINT('Ctrl Pts',(4.21062383696699E-15,-2.18004768888068,
-0.939018970625011));
#54872=CARTESIAN_POINT('Ctrl Pts',(3.77475828372553E-15,-2.13602667510567,
-1.01172829187081));
#54873=CARTESIAN_POINT('Ctrl Pts',(3.43626937052584E-15,-2.10184038761441,
-1.06819363753749));
#54874=CARTESIAN_POINT('Ctrl Pts',(3.26078485742034E-15,-2.0653368470231,
-1.12331045289651));
#54875=CARTESIAN_POINT('Ctrl Pts',(2.27595720048157E-15,-2.02662569898502,
-1.17692586826212));
#54876=CARTESIAN_POINT('Ctrl Pts',(1.80479797808039E-15,-2.0081055911475,
-1.20257644502486));
#54877=CARTESIAN_POINT('Ctrl Pts',(4.00425887293249E-15,-1.98908002883788,
-1.22788315234873));
#54878=CARTESIAN_POINT('Ctrl Pts',(3.85802501057242E-15,-1.96956020007441,
-1.2528279157208));
#54879=CARTESIAN_POINT('Ctrl Pts',(3.79622079563643E-15,-1.96131034827578,
-1.26337055948397));
#54880=CARTESIAN_POINT('Ctrl Pts',(3.69933407994927E-15,-1.95297173899764,
-1.27384911277981));
#54881=CARTESIAN_POINT('Ctrl Pts',(3.71924713249427E-15,-1.94454661500063,
-1.28426040453742));
#54882=CARTESIAN_POINT('Ctrl Pts',(3.84297659663999E-15,-1.89219722883017,
-1.34895081537832));
#54883=CARTESIAN_POINT('Ctrl Pts',(4.49708373539599E-15,-1.83671026325253,
-1.41080165676703));
#54884=CARTESIAN_POINT('Ctrl Pts',(4.08006961549745E-15,-1.77833558535246,
-1.46954266963193));
#54885=CARTESIAN_POINT('Ctrl Pts',(3.65993532101326E-15,-1.71952413762198,
-1.52872319331129));
#54886=CARTESIAN_POINT('Ctrl Pts',(3.1868423381574E-15,-1.65778083953034,
-1.58474793350827));
#54887=CARTESIAN_POINT('Ctrl Pts',(3.91353616180368E-15,-1.59333028273939,
-1.63729649350459));
#54888=CARTESIAN_POINT('Ctrl Pts',(4.60566849652001E-15,-1.53194498828118,
-1.68734584900033));
#54889=CARTESIAN_POINT('Ctrl Pts',(1.11149137391337E-15,-1.46810302924545,
-1.73424201917144));
#54890=CARTESIAN_POINT('Ctrl Pts',(3.88578058618805E-16,-1.40198217412125,
-1.77766217724644));
#54891=CARTESIAN_POINT('Ctrl Pts',(-4.44991515592973E-17,-1.36237101346623,
-1.80367398326354));
#54892=CARTESIAN_POINT('Ctrl Pts',(-6.02384006464205E-16,-1.32194172700703,
-1.82843739125673));
#54893=CARTESIAN_POINT('Ctrl Pts',(-6.66133814775094E-16,-1.28073120830839,
-1.85187402538876));
#54894=CARTESIAN_POINT('Ctrl Pts',(-6.82859527298684E-16,-1.26991901440593,
-1.85802297572131));
#54895=CARTESIAN_POINT('Ctrl Pts',(2.61624047662099E-15,-1.25905451156175,
-1.86407964602617));
#54896=CARTESIAN_POINT('Ctrl Pts',(2.58126853225349E-15,-1.2481486999723,
-1.87003721924977));
#54897=CARTESIAN_POINT('Ctrl Pts',(2.36135975416434E-15,-1.17957133762997,
-1.9074993241362));
#54898=CARTESIAN_POINT('Ctrl Pts',(3.45138597056157E-15,-1.10925109615776,
-1.94111053406059));
#54899=CARTESIAN_POINT('Ctrl Pts',(2.96984659087229E-15,-1.03737842643735,
-1.97059975361757));
#54900=CARTESIAN_POINT('Ctrl Pts',(2.77241870009471E-15,-1.00791111766478,
-1.98269013430787));
#54901=CARTESIAN_POINT('Ctrl Pts',(-2.46248839510159E-15,-0.978182658344809,
-1.99408706860885));
#54902=CARTESIAN_POINT('Ctrl Pts',(-2.41473507855972E-15,-0.94820551795056,
-2.00476939704612));
#54903=CARTESIAN_POINT('Ctrl Pts',(-2.29412135531255E-15,-0.873603723074189,
-2.03135368308536));
#54904=CARTESIAN_POINT('Ctrl Pts',(-3.153618749677E-16,-0.797461604255296,
-2.05351583539549));
#54905=CARTESIAN_POINT('Ctrl Pts',(-8.04911692853238E-16,-0.720145712205752,
-2.0713044916701));
#54906=CARTESIAN_POINT('Ctrl Pts',(-1.28269866053302E-15,-0.644687558068625,
-2.088665724031));
#54907=CARTESIAN_POINT('Ctrl Pts',(7.54333866482025E-16,-0.568110434241961,
-2.10186068177854));
#54908=CARTESIAN_POINT('Ctrl Pts',(6.24500451351651E-16,-0.490764188682584,
-2.11088835073633));
#54909=CARTESIAN_POINT('Ctrl Pts',(5.97115216600894E-16,-0.474449859358302,
-2.11279252027091));
#54910=CARTESIAN_POINT('Ctrl Pts',(2.32068381504038E-15,-0.458097295524432,
-2.11451139813136));
#54911=CARTESIAN_POINT('Ctrl Pts',(2.26207941267376E-15,-0.441737341756347,
-2.11604251162809));
#54912=CARTESIAN_POINT('Ctrl Pts',(1.98464631383226E-15,-0.364289360248237,
-2.12329079921267));
#54913=CARTESIAN_POINT('Ctrl Pts',(1.12528087701828E-16,-0.286562636972851,
-2.12635075284766));
#54914=CARTESIAN_POINT('Ctrl Pts',(2.91433543964104E-16,-0.208904513393389,
-2.12529913794706));
#54915=CARTESIAN_POINT('Ctrl Pts',(4.70215319664734E-16,-0.131300076272357,
-2.12424825004677));
#54916=CARTESIAN_POINT('Ctrl Pts',(8.34217908837847E-16,-0.0537631215199848,
-2.11909117443756));
#54917=CARTESIAN_POINT('Ctrl Pts',(7.91033905045424E-16,0.0233492957196826,
-2.10985382433648));
#54918=CARTESIAN_POINT('Ctrl Pts',(7.48568452864568E-16,0.0991786162843468,
-2.10077017727863));
#54919=CARTESIAN_POINT('Ctrl Pts',(-8.19324922797452E-17,0.174598278903728,
-2.08774052304607));
#54920=CARTESIAN_POINT('Ctrl Pts',(6.24500451351651E-17,0.249244746088756,
-2.07074577197039));
#54921=CARTESIAN_POINT('Ctrl Pts',(1.17902742706355E-16,0.277914057791417,
-2.06421863365734));
#54922=CARTESIAN_POINT('Ctrl Pts',(-2.14494948487106E-15,0.306468994429596,
-2.0571061774594));
#54923=CARTESIAN_POINT('Ctrl Pts',(-2.08166817117217E-15,0.33488758922636,
-2.04940574541392));
#54924=CARTESIAN_POINT('Ctrl Pts',(-2.05500365971468E-15,0.346862181760419,
-2.04616105521231));
#54925=CARTESIAN_POINT('Ctrl Pts',(2.87116891261715E-15,0.358812708148608,
-2.04281183170255));
#54926=CARTESIAN_POINT('Ctrl Pts',(2.94209101525666E-15,0.370723450786355,
-2.03936214920552));
#54927=CARTESIAN_POINT('Ctrl Pts',(3.37105542846375E-15,0.442764246762624,
-2.01849713007866));
#54928=CARTESIAN_POINT('Ctrl Pts',(-2.05713060706824E-15,0.513480573994915,
-1.99392658989113));
#54929=CARTESIAN_POINT('Ctrl Pts',(-1.47104550762833E-15,0.582550239122056,
-1.96568192161834));
#54930=CARTESIAN_POINT('Ctrl Pts',(-8.94437293564184E-16,0.650503060807899,
-1.93789396429752));
#54931=CARTESIAN_POINT('Ctrl Pts',(1.17556079316216E-15,0.716862809388789,
-1.90654934330102));
#54932=CARTESIAN_POINT('Ctrl Pts',(1.05124242644195E-15,0.781294350353864,
-1.87163706534072));
#54933=CARTESIAN_POINT('Ctrl Pts',(9.3090169927015E-16,0.843664366121419,
-1.83784182632811));
#54934=CARTESIAN_POINT('Ctrl Pts',(-5.67872315242143E-16,0.904228105376908,
-1.80070315888116));
#54935=CARTESIAN_POINT('Ctrl Pts',(-1.01915004213637E-15,0.962645699073296,
-1.76017850547857));
#54936=CARTESIAN_POINT('Ctrl Pts',(-1.24401152543879E-15,0.991753864592412,
-1.7399859873653));
#54937=CARTESIAN_POINT('Ctrl Pts',(3.93452992073837E-16,1.02032856987346,
-1.71895231866749));
#54938=CARTESIAN_POINT('Ctrl Pts',(4.16333634234434E-16,1.04832369103675,
-1.69706953343435));
#54939=CARTESIAN_POINT('Ctrl Pts',(-0.00732749621205394,-2.45343455551405,
-0.00158943503992818));
#54940=CARTESIAN_POINT('Ctrl Pts',(-0.00488499747470198,-2.45380114493864,
-0.0484711203631668));
#54941=CARTESIAN_POINT('Ctrl Pts',(-0.00244249873734994,-2.45277376440421,
-0.0953339889734099));
#54942=CARTESIAN_POINT('Ctrl Pts',(2.0122792321331E-15,-2.45032305592699,
-0.142102322024455));
#54943=CARTESIAN_POINT('',(-9.7495,-1.16034898466905,-1.62253437445174));
#54944=CARTESIAN_POINT('Ctrl Pts',(-9.7495,-1.16282954126729,-1.62470330690891));
#54945=CARTESIAN_POINT('Ctrl Pts',(-9.7495,-1.20725981866171,-1.60014194947285));
#54946=CARTESIAN_POINT('Ctrl Pts',(-9.7495,-1.25060328765507,-1.5738254301256));
#54947=CARTESIAN_POINT('Ctrl Pts',(-9.7495,-1.29274237783902,-1.54577696843486));
#54948=CARTESIAN_POINT('Ctrl Pts',(-9.7495,-1.3524385713109,-1.50604221411601));
#54949=CARTESIAN_POINT('Ctrl Pts',(-9.7495,-1.40971908969672,-1.462834007833));
#54950=CARTESIAN_POINT('Ctrl Pts',(-9.7495,-1.46450253747336,-1.41649569416386));
#54951=CARTESIAN_POINT('Ctrl Pts',(-9.7495,-1.49607334894272,-1.38979167636234));
#54952=CARTESIAN_POINT('Ctrl Pts',(-9.7495,-1.52681455759462,-1.36204718991875));
#54953=CARTESIAN_POINT('Ctrl Pts',(-9.7495,-1.55670736577458,-1.33332102299628));
#54954=CARTESIAN_POINT('Ctrl Pts',(-9.7495,-1.56738673003382,-1.32305844751357));
#54955=CARTESIAN_POINT('Ctrl Pts',(-9.7495,-1.57795933994072,-1.31266897018704));
#54956=CARTESIAN_POINT('Ctrl Pts',(-9.7495,-1.58841922270742,-1.30216020256279));
#54957=CARTESIAN_POINT('Ctrl Pts',(-9.7495,-1.6412280030767,-1.24910461735225));
#54958=CARTESIAN_POINT('Ctrl Pts',(-9.7495,-1.69106280077775,-1.19311726127152));
#54959=CARTESIAN_POINT('Ctrl Pts',(-9.7495,-1.73783694628383,-1.13457522246579));
#54960=CARTESIAN_POINT('Ctrl Pts',(-9.7495,-1.77722988062818,-1.08527143153372));
#54961=CARTESIAN_POINT('Ctrl Pts',(-9.7495,-1.81445176062988,-1.03415443567273));
#54962=CARTESIAN_POINT('Ctrl Pts',(-9.7495,-1.84943663148988,-0.981424505238737));
#54963=CARTESIAN_POINT('Ctrl Pts',(-9.7495,-1.86626768742428,-0.956056385056087));
#54964=CARTESIAN_POINT('Ctrl Pts',(-9.7495,-1.88258076640227,-0.930314641382609));
#54965=CARTESIAN_POINT('Ctrl Pts',(-9.7495,-1.89836721070883,-0.904220041890348));
#54966=CARTESIAN_POINT('Ctrl Pts',(-9.7495,-1.90557741537134,-0.892301753055215));
#54967=CARTESIAN_POINT('Ctrl Pts',(-9.7495,-1.9126788769199,-0.880307889440038));
#54968=CARTESIAN_POINT('Ctrl Pts',(-9.7495,-1.91966705326428,-0.868246692004634));
#54969=CARTESIAN_POINT('Ctrl Pts',(-9.7495,-1.95856708378478,-0.801107437751533));
#54970=CARTESIAN_POINT('Ctrl Pts',(-9.7495,-1.99386743501311,-0.732046302786897));
#54971=CARTESIAN_POINT('Ctrl Pts',(-9.7495,-2.02547777089641,-0.661443958471542));
#54972=CARTESIAN_POINT('Ctrl Pts',(-9.7495,-2.05827310139699,-0.588194903969676));
#54973=CARTESIAN_POINT('Ctrl Pts',(-9.7495,-2.08709738788047,-0.513286256910227));
#54974=CARTESIAN_POINT('Ctrl Pts',(-9.7495,-2.11181354003572,-0.437098919306861));
#54975=CARTESIAN_POINT('Ctrl Pts',(-9.7495,-2.13035065415217,-0.379958416104337));
#54976=CARTESIAN_POINT('Ctrl Pts',(-9.7495,-2.14657625138598,-0.32209762752316));
#54977=CARTESIAN_POINT('Ctrl Pts',(-9.7495,-2.16041564568172,-0.263665648852278));
#54978=CARTESIAN_POINT('Ctrl Pts',(-9.7495,-2.17079519140352,-0.219841664849117));
#54979=CARTESIAN_POINT('Ctrl Pts',(-9.7495,-2.17983221265302,-0.175696166465712));
#54980=CARTESIAN_POINT('Ctrl Pts',(-9.7495,-2.18748897925106,-0.131289748942107));
#54981=CARTESIAN_POINT('Ctrl Pts',(-9.7495,-2.18975737345239,-0.118133900618595));
#54982=CARTESIAN_POINT('Ctrl Pts',(-9.7495,-2.19190458459009,-0.104955142021024));
#54983=CARTESIAN_POINT('Ctrl Pts',(-9.7495,-2.19392953304095,-0.0917550286362238));
#54984=CARTESIAN_POINT('Ctrl Pts',(-9.7495,-2.19598691316673,-0.0783435015801452));
#54985=CARTESIAN_POINT('Ctrl Pts',(-9.7495,-2.19791670474282,-0.0649186893148607));
#54986=CARTESIAN_POINT('Ctrl Pts',(-9.7495,-2.19971761564778,-0.0514875996340031));
#54987=CARTESIAN_POINT('Ctrl Pts',(-9.7495,-2.21048362106498,0.0288046479531155));
#54988=CARTESIAN_POINT('Ctrl Pts',(-9.7495,-2.21665631602757,0.109377787870744));
#54989=CARTESIAN_POINT('Ctrl Pts',(-9.7495,-2.21810551533992,0.189856369992003));
#54990=CARTESIAN_POINT('Ctrl Pts',(-9.7495,-2.21859139159652,0.216838602101243));
#54991=CARTESIAN_POINT('Ctrl Pts',(-9.7495,-2.21854594662738,0.243810439064412));
#54992=CARTESIAN_POINT('Ctrl Pts',(-9.7495,-2.21796310993972,0.270758339650537));
#54993=CARTESIAN_POINT('Ctrl Pts',(-9.7495,-2.21628399885951,0.34839332629562));
#54994=CARTESIAN_POINT('Ctrl Pts',(-9.7495,-2.21014862867717,0.42582911455849));
#54995=CARTESIAN_POINT('Ctrl Pts',(-9.7495,-2.19978974399978,0.502815302022679));
#54996=CARTESIAN_POINT('Ctrl Pts',(-9.7495,-2.18921662014655,0.581393693461284));
#54997=CARTESIAN_POINT('Ctrl Pts',(-9.7495,-2.17424335640218,0.659504469453206));
#54998=CARTESIAN_POINT('Ctrl Pts',(-9.7495,-2.15506353264355,0.736883240528982));
#54999=CARTESIAN_POINT('Ctrl Pts',(-9.7495,-2.15038816510247,0.755745467794927));
#55000=CARTESIAN_POINT('Ctrl Pts',(-9.7495,-2.14546061333694,0.774570849813381));
#55001=CARTESIAN_POINT('Ctrl Pts',(-9.7495,-2.14029345944492,0.793319915467821));
#55002=CARTESIAN_POINT('Ctrl Pts',(-9.7495,-2.11879135289761,0.871340507807307));
#55003=CARTESIAN_POINT('Ctrl Pts',(-9.7495,-2.09312591146214,0.948126958360234));
#55004=CARTESIAN_POINT('Ctrl Pts',(-9.7495,-2.06357340075898,1.02340971215714));
#55005=CARTESIAN_POINT('Ctrl Pts',(-9.7495,-2.03343217208749,1.10019217981288));
#55006=CARTESIAN_POINT('Ctrl Pts',(-9.7495,-1.99924727417101,1.17541126817356));
#55007=CARTESIAN_POINT('Ctrl Pts',(-9.7495,-1.96125645040679,1.24878274079809));
#55008=CARTESIAN_POINT('Ctrl Pts',(-9.7495,-1.92297082575374,1.32272356078602));
#55009=CARTESIAN_POINT('Ctrl Pts',(-9.7495,-1.88081965493645,1.39478889359068));
#55010=CARTESIAN_POINT('Ctrl Pts',(-9.7495,-1.83499464778345,1.46467637745762));
#55011=CARTESIAN_POINT('Ctrl Pts',(-9.7495,-1.8155367458887,1.49435152404764));
#55012=CARTESIAN_POINT('Ctrl Pts',(-9.7495,-1.79541586112841,1.52363379132999));
#55013=CARTESIAN_POINT('Ctrl Pts',(-9.7495,-1.77464411274757,1.55249878188989));
#55014=CARTESIAN_POINT('Ctrl Pts',(-9.7495,-1.76421881478994,1.56698606151671));
#55015=CARTESIAN_POINT('Ctrl Pts',(-9.7495,-1.75362655654722,1.58137198762931));
#55016=CARTESIAN_POINT('Ctrl Pts',(-9.7495,-1.74288704456025,1.59562963858262));
#55017=CARTESIAN_POINT('Ctrl Pts',(-9.7495,-1.69123008364333,1.66420881787453));
#55018=CARTESIAN_POINT('Ctrl Pts',(-9.7495,-1.63610306663109,1.72991874708502));
#55019=CARTESIAN_POINT('Ctrl Pts',(-9.7495,-1.57776314502671,1.79246368429379));
#55020=CARTESIAN_POINT('Ctrl Pts',(-9.7495,-1.51932766137129,1.85511107145994));
#55021=CARTESIAN_POINT('Ctrl Pts',(-9.7495,-1.45766830476388,1.91458402426312));
#55022=CARTESIAN_POINT('Ctrl Pts',(-9.7495,-1.39299427766318,1.97056794509669));
#55023=CARTESIAN_POINT('Ctrl Pts',(-9.7495,-1.32968169197049,2.02537335839916));
#55024=CARTESIAN_POINT('Ctrl Pts',(-9.7495,-1.263479463329,2.07683587217845));
#55025=CARTESIAN_POINT('Ctrl Pts',(-9.7495,-1.19454434316117,2.12463112085497));
#55026=CARTESIAN_POINT('Ctrl Pts',(-9.7495,-1.15559117428643,2.15163878238619));
#55027=CARTESIAN_POINT('Ctrl Pts',(-9.7495,-1.11576470790424,2.17747487576121));
#55028=CARTESIAN_POINT('Ctrl Pts',(-9.7495,-1.07508846035131,2.20207516956607));
#55029=CARTESIAN_POINT('Ctrl Pts',(-9.7495,-1.16282954126728,-1.62470330690891));
#55030=CARTESIAN_POINT('Ctrl Pts',(-9.7104670095946,-0.665448492800351,
-1.9765110105703));
#55031=CARTESIAN_POINT('Ctrl Pts',(-9.62918664625593,0.733870831796914,
-2.20998455802869));
#55032=CARTESIAN_POINT('Ctrl Pts',(-9.50565890998404,2.2663578788523,-0.643561605617013));
#55033=CARTESIAN_POINT('Ctrl Pts',(-9.37891679118423,1.77297281393676,1.55184140168292));
#55034=CARTESIAN_POINT('Ctrl Pts',(-9.25217467238445,-0.337135258971208,
2.331634562323));
#55035=CARTESIAN_POINT('Ctrl Pts',(-9.14935403578811,-1.7995037137583,1.24001182649284));
#55036=CARTESIAN_POINT('Ctrl Pts',(-9.08878077212504,-1.99264490228889,
0.288835621098305));
#55037=CARTESIAN_POINT('Ctrl Pts',(-9.07045488139523,-1.99173797669883,
0.000711821429190372));
#55038=CARTESIAN_POINT('Origin',(-9.7495,-5.69858952725515E-16,8.58067791224701E-17));
#55039=CARTESIAN_POINT('',(-9.7495,-2.4505,-3.00099698131059E-16));
#55040=CARTESIAN_POINT('Origin',(-9.7495,0.,0.));
#55041=CARTESIAN_POINT('Origin',(-9.7495,0.,0.));
#55042=CARTESIAN_POINT('',(-9.7495,1.16034898466907,-1.62253437445173));
#55043=CARTESIAN_POINT('Ctrl Pts',(-9.7495,1.07765198048948,2.20520778639847));
#55044=CARTESIAN_POINT('Ctrl Pts',(-9.7495,1.13060525254771,2.17351956564304));
#55045=CARTESIAN_POINT('Ctrl Pts',(-9.7495,1.18219250140317,2.13974889587976));
#55046=CARTESIAN_POINT('Ctrl Pts',(-9.7495,1.23227301946895,2.10388882904113));
#55047=CARTESIAN_POINT('Ctrl Pts',(-9.7495,1.30160344320515,2.0542449011196));
#55048=CARTESIAN_POINT('Ctrl Pts',(-9.7495,1.36804803363604,2.00059746133367));
#55049=CARTESIAN_POINT('Ctrl Pts',(-9.7495,1.43143746154022,1.94330837559225));
#55050=CARTESIAN_POINT('Ctrl Pts',(-9.7495,1.46335696993216,1.91446067158941));
#55051=CARTESIAN_POINT('Ctrl Pts',(-9.7495,1.4945011602568,1.88468908019348));
#55052=CARTESIAN_POINT('Ctrl Pts',(-9.7495,1.52484417134257,1.85403731928515));
#55053=CARTESIAN_POINT('Ctrl Pts',(-9.7495,1.53884696008258,1.83989204770035));
#55054=CARTESIAN_POINT('Ctrl Pts',(-9.7495,1.55267908267023,1.82555931105367));
#55055=CARTESIAN_POINT('Ctrl Pts',(-9.7495,1.56633777788309,1.81104332574806));
#55056=CARTESIAN_POINT('Ctrl Pts',(-9.7495,1.57690316529314,1.7998148001823));
#55057=CARTESIAN_POINT('Ctrl Pts',(-9.7495,1.58736167323699,1.78847985698288));
#55058=CARTESIAN_POINT('Ctrl Pts',(-9.7495,1.59770709521557,1.7770464269894));
#55059=CARTESIAN_POINT('Ctrl Pts',(-9.7495,1.65468948937111,1.71407130468052));
#55060=CARTESIAN_POINT('Ctrl Pts',(-9.7495,1.70829401366604,1.64805835503819));
#55061=CARTESIAN_POINT('Ctrl Pts',(-9.7495,1.75835312501744,1.57936654442874));
#55062=CARTESIAN_POINT('Ctrl Pts',(-9.7495,1.79722852674469,1.52602117610869));
#55063=CARTESIAN_POINT('Ctrl Pts',(-9.7495,1.83396491012993,1.47105939656799));
#55064=CARTESIAN_POINT('Ctrl Pts',(-9.7495,1.8684636308021,1.41464139286296));
#55065=CARTESIAN_POINT('Ctrl Pts',(-9.7495,1.88496848237078,1.38764993466363));
#55066=CARTESIAN_POINT('Ctrl Pts',(-9.7495,1.90096089521604,1.36032509902764));
#55067=CARTESIAN_POINT('Ctrl Pts',(-9.7495,1.91642851998693,1.33268418774228));
#55068=CARTESIAN_POINT('Ctrl Pts',(-9.7495,1.9229656492837,1.32100222534473));
#55069=CARTESIAN_POINT('Ctrl Pts',(-9.7495,1.92940937815796,1.30926315589405));
#55070=CARTESIAN_POINT('Ctrl Pts',(-9.7495,1.93575764807029,1.29747027314868));
#55071=CARTESIAN_POINT('Ctrl Pts',(-9.7495,1.97520304718045,1.22419440854714));
#55072=CARTESIAN_POINT('Ctrl Pts',(-9.7495,2.01081723995188,1.14912148554907));
#55073=CARTESIAN_POINT('Ctrl Pts',(-9.7495,2.04244747514414,1.07258637442353));
#55074=CARTESIAN_POINT('Ctrl Pts',(-9.7495,2.07431436729968,0.995478628700962));
#55075=CARTESIAN_POINT('Ctrl Pts',(-9.7495,2.10213786509534,0.916885736586536));
#55076=CARTESIAN_POINT('Ctrl Pts',(-9.7495,2.12570920792973,0.837138623357578));
#55077=CARTESIAN_POINT('Ctrl Pts',(-9.7495,2.14815951980743,0.761184208035744));
#55078=CARTESIAN_POINT('Ctrl Pts',(-9.7495,2.16675239673109,0.68418193503517));
#55079=CARTESIAN_POINT('Ctrl Pts',(-9.7495,2.18125874771835,0.606420481194756));
#55080=CARTESIAN_POINT('Ctrl Pts',(-9.7495,2.18994910664117,0.559835716712814));
#55081=CARTESIAN_POINT('Ctrl Pts',(-9.7495,2.19717192894386,0.512978600722697));
#55082=CARTESIAN_POINT('Ctrl Pts',(-9.7495,2.20286917549892,0.465913439685798));
#55083=CARTESIAN_POINT('Ctrl Pts',(-9.7495,2.2043639310029,0.453565210093529));
#55084=CARTESIAN_POINT('Ctrl Pts',(-9.7495,2.20575336285344,0.441204380991941));
#55085=CARTESIAN_POINT('Ctrl Pts',(-9.7495,2.20703543274385,0.428843731680537));
#55086=CARTESIAN_POINT('Ctrl Pts',(-9.7495,2.215097279967,0.35111812009494));
#55087=CARTESIAN_POINT('Ctrl Pts',(-9.7495,2.21893389153702,0.273272553006201));
#55088=CARTESIAN_POINT('Ctrl Pts',(-9.7495,2.21836879129015,0.195587420768878));
#55089=CARTESIAN_POINT('Ctrl Pts',(-9.7495,2.21813710572717,0.163737277900239));
#55090=CARTESIAN_POINT('Ctrl Pts',(-9.7495,2.21716493310934,0.131914139447269));
#55091=CARTESIAN_POINT('Ctrl Pts',(-9.7495,2.21543757405891,0.100137680361018));
#55092=CARTESIAN_POINT('Ctrl Pts',(-9.7495,2.21113879773801,0.0210574857432948));
#55093=CARTESIAN_POINT('Ctrl Pts',(-9.7495,2.20216614528477,-0.0577351639422519));
#55094=CARTESIAN_POINT('Ctrl Pts',(-9.7495,2.1887060785629,-0.135920959021978));
#55095=CARTESIAN_POINT('Ctrl Pts',(-9.7495,2.17556943398582,-0.212228084548267));
#55096=CARTESIAN_POINT('Ctrl Pts',(-9.7495,2.15815768408866,-0.287957857661971));
#55097=CARTESIAN_POINT('Ctrl Pts',(-9.7495,2.13660504087781,-0.362787194479743));
#55098=CARTESIAN_POINT('Ctrl Pts',(-9.7495,2.13205903634164,-0.378570618409907));
#55099=CARTESIAN_POINT('Ctrl Pts',(-9.7495,2.12732735489629,-0.394317729407546));
#55100=CARTESIAN_POINT('Ctrl Pts',(-9.7495,2.12241963127094,-0.40999912220641));
#55101=CARTESIAN_POINT('Ctrl Pts',(-9.7495,2.09918643850731,-0.484234928765601));
#55102=CARTESIAN_POINT('Ctrl Pts',(-9.7495,2.07198237645875,-0.557109856056304));
#55103=CARTESIAN_POINT('Ctrl Pts',(-9.7495,2.04101243041346,-0.628333178632409));
#55104=CARTESIAN_POINT('Ctrl Pts',(-9.7495,2.01006390965093,-0.699507228283652));
#55105=CARTESIAN_POINT('Ctrl Pts',(-9.7495,1.97535404006358,-0.769032784087818));
#55106=CARTESIAN_POINT('Ctrl Pts',(-9.7495,1.93704465465342,-0.836590516839988));
#55107=CARTESIAN_POINT('Ctrl Pts',(-9.7495,1.8993727277891,-0.903024105896846));
#55108=CARTESIAN_POINT('Ctrl Pts',(-9.7495,1.85821938417217,-0.96755546663314));
#55109=CARTESIAN_POINT('Ctrl Pts',(-9.7495,1.81370745162356,-1.02984190631639));
#55110=CARTESIAN_POINT('Ctrl Pts',(-9.7495,1.79661180052436,-1.05376419366874));
#55111=CARTESIAN_POINT('Ctrl Pts',(-9.7495,1.77902045192394,-1.07735487007615));
#55112=CARTESIAN_POINT('Ctrl Pts',(-9.7495,1.76093944008161,-1.10059264695084));
#55113=CARTESIAN_POINT('Ctrl Pts',(-9.7495,1.75332075268837,-1.11038420946216));
#55114=CARTESIAN_POINT('Ctrl Pts',(-9.7495,1.74561494379555,-1.12011319186763));
#55115=CARTESIAN_POINT('Ctrl Pts',(-9.7495,1.73783184327634,-1.12976667062739));
#55116=CARTESIAN_POINT('Ctrl Pts',(-9.7495,1.69075667140557,-1.18815460621232));
#55117=CARTESIAN_POINT('Ctrl Pts',(-9.7495,1.64077529421437,-1.2438894167514));
#55118=CARTESIAN_POINT('Ctrl Pts',(-9.7495,1.58804113169155,-1.29668604581243));
#55119=CARTESIAN_POINT('Ctrl Pts',(-9.7495,1.53615968694636,-1.34862894700437));
#55120=CARTESIAN_POINT('Ctrl Pts',(-9.7495,1.48161310229243,-1.39772847498648));
#55121=CARTESIAN_POINT('Ctrl Pts',(-9.7495,1.42452070117096,-1.44367126303871));
#55122=CARTESIAN_POINT('Ctrl Pts',(-9.7495,1.36925502008041,-1.48814407243243));
#55123=CARTESIAN_POINT('Ctrl Pts',(-9.7495,1.31160324244574,-1.52965923065524));
#55124=CARTESIAN_POINT('Ctrl Pts',(-9.7495,1.25165740686919,-1.56788681092577));
#55125=CARTESIAN_POINT('Ctrl Pts',(-9.7495,1.22178755544821,-1.58693487543071));
#55126=CARTESIAN_POINT('Ctrl Pts',(-9.7495,1.19134792456383,-1.60516593716848));
#55127=CARTESIAN_POINT('Ctrl Pts',(-9.7495,1.16034898466909,-1.62253437445172));
#55128=CARTESIAN_POINT('Origin',(-9.7495,0.,0.));
#55129=CARTESIAN_POINT('Origin',(-11.2285451186048,0.,0.));
#55130=CARTESIAN_POINT('Ctrl Pts',(-9.7495,1.16034898466907,-1.62253437445173));
#55131=CARTESIAN_POINT('Ctrl Pts',(-9.70725262706674,1.69872226327124,-1.23751887213913));
#55132=CARTESIAN_POINT('Ctrl Pts',(-9.62275788120021,2.35301974079721,0.103728689921924));
#55133=CARTESIAN_POINT('Ctrl Pts',(-9.49601576240043,1.19113795339939,2.03448789178737));
#55134=CARTESIAN_POINT('Ctrl Pts',(-9.36927364360064,-1.05771687947754,
2.10445274652685));
#55135=CARTESIAN_POINT('Ctrl Pts',(-9.28011676233542,-1.96094440164537,
0.806069483628623));
#55136=CARTESIAN_POINT('Ctrl Pts',(-9.23320725400347,-1.99753352956653,
0.0741460916094852));
#55137=CARTESIAN_POINT('Ctrl Pts',(-9.22854511860477,-1.99701091303081,
0.00134739702958217));
#55138=CARTESIAN_POINT('Ctrl Pts',(-10.0126273851832,1.42545942445495,-1.99324250386965));
#55139=CARTESIAN_POINT('Ctrl Pts',(-9.97038001224991,2.08683740125135,-1.52026068237975));
#55140=CARTESIAN_POINT('Ctrl Pts',(-9.88588526638338,2.89062532890015,0.127428076026371));
#55141=CARTESIAN_POINT('Ctrl Pts',(-9.75914314758361,1.46328289500202,2.49931699652835));
#55142=CARTESIAN_POINT('Ctrl Pts',(-9.63240102878381,-1.2993784750769,2.58526705369799));
#55143=CARTESIAN_POINT('Ctrl Pts',(-9.50565890998404,-2.8767336334322,0.317830015974396));
#55144=CARTESIAN_POINT('Ctrl Pts',(-9.37891679118423,-1.83166120490144,
-2.24126795020257));
#55145=CARTESIAN_POINT('Ctrl Pts',(-9.25217467238446,0.883542867790515,
-2.75597710770364));
#55146=CARTESIAN_POINT('Ctrl Pts',(-9.12543255358466,2.79311408050666,-0.758535600360605));
#55147=CARTESIAN_POINT('Ctrl Pts',(-8.99869043478488,2.15620672142397,1.93074660360672));
#55148=CARTESIAN_POINT('Ctrl Pts',(-8.8719483159851,-0.446574495801375,
2.8595936543393));
#55149=CARTESIAN_POINT('Ctrl Pts',(-8.7452061971853,-2.64219320892422,1.1813777274502));
#55150=CARTESIAN_POINT('Ctrl Pts',(-8.61846407838552,-2.42888879364233,
-1.57395843532259));
#55151=CARTESIAN_POINT('Ctrl Pts',(-8.49172195958573,-0.00112366212568968,
-2.89427081971438));
#55152=CARTESIAN_POINT('Ctrl Pts',(-8.36497984078595,2.4276640081396,-1.5758406156409));
#55153=CARTESIAN_POINT('Ctrl Pts',(-8.23823772198616,2.64311229295518,1.17931450649545));
#55154=CARTESIAN_POINT('Ctrl Pts',(-8.11149560318636,0.448791983620454,
2.85926663546641));
#55155=CARTESIAN_POINT('Ctrl Pts',(-7.98475348438658,-2.15469893161674,
1.93238085090762));
#55156=CARTESIAN_POINT('Ctrl Pts',(-7.85801136558679,-2.79371625747268,
-0.756288504049397));
#55157=CARTESIAN_POINT('Ctrl Pts',(-7.73126924678701,-0.885657380199097,
-2.7554370180037));
#55158=CARTESIAN_POINT('Ctrl Pts',(-7.60452712798722,1.82986956127592,-2.24240942758177));
#55159=CARTESIAN_POINT('Ctrl Pts',(-7.47778500918743,2.87707496001139,0.315059086878021));
#55160=CARTESIAN_POINT('Ctrl Pts',(-7.35104289038765,1.3012047485017,2.58528309394231));
#55161=CARTESIAN_POINT('Ctrl Pts',(-7.22430077158787,-1.46099479274749,
2.49846287982005));
#55162=CARTESIAN_POINT('Ctrl Pts',(-7.09755865278807,-2.89118184349023,
0.133753783635275));
#55163=CARTESIAN_POINT('Ctrl Pts',(-6.97081653398828,-1.68543182040245,
-2.35290078342189));
#55164=CARTESIAN_POINT('Ctrl Pts',(-6.8440744151885,1.05695354983856,-2.69437779863599));
#55165=CARTESIAN_POINT('Ctrl Pts',(-6.71733229638871,2.83569733845996,-0.579347157962499));
#55166=CARTESIAN_POINT('Ctrl Pts',(-6.59059017758893,2.02909017185975,2.06388362035805));
#55167=CARTESIAN_POINT('Ctrl Pts',(-6.46384805878913,-0.627471198984668,
2.82543844736086));
#55168=CARTESIAN_POINT('Ctrl Pts',(-6.33710593998935,-2.71195696734964,
1.01099551533597));
#55169=CARTESIAN_POINT('Ctrl Pts',(-6.21036382118956,-2.32390787085462,
-1.72518831798258));
#55170=CARTESIAN_POINT('Ctrl Pts',(-6.08362170238978,0.182885476550568,
-2.88849016397656));
#55171=CARTESIAN_POINT('Ctrl Pts',(-5.95687958358999,2.52293918816451,-1.41830898525316));
#55172=CARTESIAN_POINT('Ctrl Pts',(-5.8301374647902,2.56278858986834,1.34496734847618));
#55173=CARTESIAN_POINT('Ctrl Pts',(-5.70339534599041,0.266102340043448,
2.88201527918852));
#55174=CARTESIAN_POINT('Ctrl Pts',(-5.57665322719064,-2.27319370090067,
1.79148344201757));
#55175=CARTESIAN_POINT('Ctrl Pts',(-5.44991110839083,-2.73998241681994,
-0.932372715364727));
#55176=CARTESIAN_POINT('Ctrl Pts',(-5.32316898959106,-0.708685014056901,
-2.80616964485284));
#55177=CARTESIAN_POINT('Ctrl Pts',(-5.19642687079127,1.9687319350458,-2.12153649338652));
#55178=CARTESIAN_POINT('Ctrl Pts',(-5.06968475199148,2.85122425683898,0.497335663363999));
#55179=CARTESIAN_POINT('Ctrl Pts',(-4.94294263319169,1.13420948196707,2.66277888226879));
#55180=CARTESIAN_POINT('Ctrl Pts',(-4.81620051439191,-1.61688235310285,
2.40052368891968));
#55181=CARTESIAN_POINT('Ctrl Pts',(-4.68945839559212,-2.89383649406469,
-0.0503276311953479));
#55182=CARTESIAN_POINT('Ctrl Pts',(-4.56271627679233,-1.5324332750719,-2.45529443902181));
#55183=CARTESIAN_POINT('Ctrl Pts',(-4.43597415799255,1.22611405286081,-2.62172974469429));
#55184=CARTESIAN_POINT('Ctrl Pts',(-4.30923203919275,2.86679344245922,-0.397891798263646));
#55185=CARTESIAN_POINT('Ctrl Pts',(-4.18248992039298,1.89377105798942,2.18871051186493));
#55186=CARTESIAN_POINT('Ctrl Pts',(-4.05574780159318,-0.805832914320809,
2.77983018168796));
#55187=CARTESIAN_POINT('Ctrl Pts',(-3.9290056827934,-2.77074603430605,0.836533883533555));
#55188=CARTESIAN_POINT('Ctrl Pts',(-3.80226356399361,-2.209525349802,-1.86944383529057));
#55189=CARTESIAN_POINT('Ctrl Pts',(-3.67552144519382,0.366155198045445,
-2.87101948717351));
#55190=CARTESIAN_POINT('Ctrl Pts',(-3.54877932639404,2.60800615217148,-1.25504041194532));
#55191=CARTESIAN_POINT('Ctrl Pts',(-3.42203720759424,2.47209587427006,1.50517922930694));
#55192=CARTESIAN_POINT('Ctrl Pts',(-3.29529508879447,0.0823359556551343,
2.89310271424892));
#55193=CARTESIAN_POINT('Ctrl Pts',(-3.16855296999467,-2.38249098169967,
1.64333783818743));
#55194=CARTESIAN_POINT('Ctrl Pts',(-3.04181085119489,-2.67516249955718,
-1.10468462414187));
#55195=CARTESIAN_POINT('Ctrl Pts',(-2.9150687323951,-0.528845266442932,
-2.84554831463556));
#55196=CARTESIAN_POINT('Ctrl Pts',(-2.78832661359532,2.09962872632452,-1.99207975690403));
#55197=CARTESIAN_POINT('Ctrl Pts',(-2.66158449479553,2.81383736093294,0.677600014437121));
#55198=CARTESIAN_POINT('Ctrl Pts',(-2.53484237599574,0.962625166914014,
2.72950093272979));
#55199=CARTESIAN_POINT('Ctrl Pts',(-2.40810025719596,-1.76622796476978,
2.29287187358059));
#55200=CARTESIAN_POINT('Ctrl Pts',(-2.28135813839617,-2.88478248307408,
-0.23420542400883));
#55201=CARTESIAN_POINT('Ctrl Pts',(-2.15461601959638,-1.37323455557573,
-2.5477538507472));
#55202=CARTESIAN_POINT('Ctrl Pts',(-2.02787390079659,1.39031387507737,-2.53847406282439));
#55203=CARTESIAN_POINT('Ctrl Pts',(-1.9011317819968,2.88628991979766,-0.214826525661565));
#55204=CARTESIAN_POINT('Ctrl Pts',(-1.77438966319702,1.75079050957589,2.30468173290378));
#55205=CARTESIAN_POINT('Ctrl Pts',(-1.64764754439723,-0.980935816608061,
2.72297467965007));
#55206=CARTESIAN_POINT('Ctrl Pts',(-1.52090542559744,-2.81832143441497,
0.6586874317792));
#55207=CARTESIAN_POINT('Ctrl Pts',(-1.39416330679766,-2.08620889714375,
-2.0061351812584));
#55208=CARTESIAN_POINT('Ctrl Pts',(-1.26742118799787,0.54795471416747,-2.84193313070915));
#55209=CARTESIAN_POINT('Ctrl Pts',(-1.14067906919808,2.682499493013,-1.0866927432457));
#55210=CARTESIAN_POINT('Ctrl Pts',(-1.0139369503983,2.37144197069276,1.65929890390176));
#55211=CARTESIAN_POINT('Ctrl Pts',(-0.887194831598508,-0.101841824517894,
2.89248868044766));
#55212=CARTESIAN_POINT('Ctrl Pts',(-0.760452712798723,-2.48199930473078,
1.48853527627866));
#55213=CARTESIAN_POINT('Ctrl Pts',(-0.633710593998933,-2.59980356409773,
-1.27251177686141));
#55214=CARTESIAN_POINT('Ctrl Pts',(-0.506968475199149,-0.346322090654253,
-2.8734427654469));
#55215=CARTESIAN_POINT('Ctrl Pts',(-0.380226356399359,2.22098961772557,
-1.85450674800193));
#55216=CARTESIAN_POINT('Ctrl Pts',(-0.253484237599575,2.76708226469713,
0.855007614199791));
#55217=CARTESIAN_POINT('Ctrl Pts',(-0.126742118799785,0.783023399402025,
2.78546711749175));
#55218=CARTESIAN_POINT('Ctrl Pts',(-0.0422473729332622,-1.00451454043688,
2.37845189560396));
#55219=CARTESIAN_POINT('Ctrl Pts',(0.,-1.6158113816168,1.84230937386683));
#55220=CARTESIAN_POINT('Ctrl Pts',(-9.92491825678878,1.33708927785966,-1.86967312739701));
#55221=CARTESIAN_POINT('Ctrl Pts',(-9.88267088385552,1.95746568859131,-1.42601341229954));
#55222=CARTESIAN_POINT('Ctrl Pts',(-9.79817613798899,2.71142346619917,0.119528280658224));
#55223=CARTESIAN_POINT('Ctrl Pts',(-9.67143401918922,1.37256791446781,2.34437396161469));
#55224=CARTESIAN_POINT('Ctrl Pts',(-9.54469190038942,-1.21882460987711,
2.42499561797428));
#55225=CARTESIAN_POINT('Ctrl Pts',(-9.41794978158964,-2.69839297459568,
0.298126414018276));
#55226=CARTESIAN_POINT('Ctrl Pts',(-9.29120766278985,-1.71810892385214,
-2.10232244679445));
#55227=CARTESIAN_POINT('Ctrl Pts',(-9.16446554399006,0.828768377959128,
-2.58512264713969));
#55228=CARTESIAN_POINT('Ctrl Pts',(-9.03772342519027,2.61995734484851,-0.711510829924037));
#55229=CARTESIAN_POINT('Ctrl Pts',(-8.91098130639049,2.02253451666453,1.81105160740271));
#55230=CARTESIAN_POINT('Ctrl Pts',(-8.7842391875907,-0.418889489141318,
2.68231557395229));
#55231=CARTESIAN_POINT('Ctrl Pts',(-8.65749706879092,-2.4783926845459,1.10813921839959));
#55232=CARTESIAN_POINT('Ctrl Pts',(-8.53075494999112,-2.27831189536272,
-1.47638221864597));
#55233=CARTESIAN_POINT('Ctrl Pts',(-8.40401283119134,-0.00105400164635133,
-2.71484295790593));
#55234=CARTESIAN_POINT('Ctrl Pts',(-8.27727071239155,2.27716303939722,-1.47814771479367));
#55235=CARTESIAN_POINT('Ctrl Pts',(-8.15052859359177,2.47925479074279,1.10620390507598));
#55236=CARTESIAN_POINT('Ctrl Pts',(-8.02378647479198,0.420969505686005,
2.68200882833674));
#55237=CARTESIAN_POINT('Ctrl Pts',(-7.8970443559922,-2.02112020100608,1.81258454092991));
#55238=CARTESIAN_POINT('Ctrl Pts',(-7.7703022371924,-2.62052219036486,-0.709403040440553));
#55239=CARTESIAN_POINT('Ctrl Pts',(-7.64356011839262,-0.830751802966448,
-2.58461603984207));
#55240=CARTESIAN_POINT('Ctrl Pts',(-7.51681799959283,1.71642835165184,-2.1033931592528));
#55241=CARTESIAN_POINT('Ctrl Pts',(-7.39007588079305,2.69871314092343,0.29552726631833));
#55242=CARTESIAN_POINT('Ctrl Pts',(-7.26333376199325,1.2205376650317,2.42501066381727));
#55243=CARTESIAN_POINT('Ctrl Pts',(-7.13659164319347,-1.37042166116963,
2.34357279514644));
#55244=CARTESIAN_POINT('Ctrl Pts',(-7.00984952439368,-2.71194548013981,
0.125461831395346));
#55245=CARTESIAN_POINT('Ctrl Pts',(-6.8831074055939,-1.58094490587501,-2.20703469731096));
#55246=CARTESIAN_POINT('Ctrl Pts',(-6.75636528679411,0.99142861202466,-2.52734213493084));
#55247=CARTESIAN_POINT('Ctrl Pts',(-6.62962316799432,2.65990068988442,-0.543431022855178));
#55248=CARTESIAN_POINT('Ctrl Pts',(-6.50288104919453,1.90329844964998,1.93593490785338));
#55249=CARTESIAN_POINT('Ctrl Pts',(-6.37613893039475,-0.588571654818552,
2.6502777900277));
#55250=CARTESIAN_POINT('Ctrl Pts',(-6.24939681159495,-2.54383149800739,
0.948319706845946));
#55251=CARTESIAN_POINT('Ctrl Pts',(-6.12265469279518,-2.17983917573905,
-1.61823673314677));
#55252=CARTESIAN_POINT('Ctrl Pts',(-5.99591257399538,0.171547646728372,
-2.70942066901194));
#55253=CARTESIAN_POINT('Ctrl Pts',(-5.8691704551956,2.36653171553907,-1.3303821240644));
#55254=CARTESIAN_POINT('Ctrl Pts',(-5.74242833639581,2.40391068742223,1.26158723978164));
#55255=CARTESIAN_POINT('Ctrl Pts',(-5.61568621759602,0.2496055514323,2.70334718920823));
#55256=CARTESIAN_POINT('Ctrl Pts',(-5.48894409879623,-2.13226898768766,
1.68042194726145));
#55257=CARTESIAN_POINT('Ctrl Pts',(-5.36220197999646,-2.57011953353548,
-0.874571060596665));
#55258=CARTESIAN_POINT('Ctrl Pts',(-5.23545986119665,-0.664750688387785,
-2.63220354056913));
#55259=CARTESIAN_POINT('Ctrl Pts',(-5.10871774239688,1.84668207047434,-1.99001363997416));
#55260=CARTESIAN_POINT('Ctrl Pts',(-4.98197562359709,2.67446503014315,0.466503761224565));
#55261=CARTESIAN_POINT('Ctrl Pts',(-4.85523350479731,1.06389512824245,2.49770216655173));
#55262=CARTESIAN_POINT('Ctrl Pts',(-4.72849138599751,-1.51664510459213,
2.25170526122123));
#55263=CARTESIAN_POINT('Ctrl Pts',(-4.60174926719773,-2.71443555790608,
-0.0472076124349324));
#55264=CARTESIAN_POINT('Ctrl Pts',(-4.47500714839794,-1.43743137544406,
-2.30308054517917));
#55265=CARTESIAN_POINT('Ctrl Pts',(-4.34826502959816,1.15010215330408,-2.45919783540443));
#55266=CARTESIAN_POINT('Ctrl Pts',(-4.22152291079836,2.68906901732139,-0.373224834098681));
#55267=CARTESIAN_POINT('Ctrl Pts',(-4.09478079199859,1.77636832933829,2.05302326221759));
#55268=CARTESIAN_POINT('Ctrl Pts',(-3.96803867319879,-0.755875987067642,
2.60749697005709));
#55269=CARTESIAN_POINT('Ctrl Pts',(-3.84129655439901,-2.59897598667836,
0.784673675763648));
#55270=CARTESIAN_POINT('Ctrl Pts',(-3.71455443559922,-2.07254770195159,
-1.75354925215331));
#55271=CARTESIAN_POINT('Ctrl Pts',(-3.58781231679943,0.343455717462007,
-2.69303307198214));
#55272=CARTESIAN_POINT('Ctrl Pts',(-3.46107019799965,2.44632502534674,-1.17723524731985));
#55273=CARTESIAN_POINT('Ctrl Pts',(-3.33432807919985,2.31884038971607,1.41186692110364));
#55274=CARTESIAN_POINT('Ctrl Pts',(-3.20758596040008,0.0772316079995686,
2.71374726814691));
#55275=CARTESIAN_POINT('Ctrl Pts',(-3.08084384160028,-2.23479047637292,
1.54146050434346));
#55276=CARTESIAN_POINT('Ctrl Pts',(-2.9541017228005,-2.50931807200182,-1.03620063890721));
#55277=CARTESIAN_POINT('Ctrl Pts',(-2.82735960400071,-0.496059953216865,
-2.66914096315693));
#55278=CARTESIAN_POINT('Ctrl Pts',(-2.70061748520092,1.96946402632828,-1.86858246394218));
#55279=CARTESIAN_POINT('Ctrl Pts',(-2.57387536640114,2.63939590310186,0.635592776923738));
#55280=CARTESIAN_POINT('Ctrl Pts',(-2.44713324760135,0.902948037100895,
2.56028784015119));
#55281=CARTESIAN_POINT('Ctrl Pts',(-2.32039112880156,-1.65673216188006,
2.15072722876193));
#55282=CARTESIAN_POINT('Ctrl Pts',(-2.19364901000178,-2.70594284263865,
-0.219686057622113));
#55283=CARTESIAN_POINT('Ctrl Pts',(-2.06690689120199,-1.28810204538003,
-2.38980801418622));
#55284=CARTESIAN_POINT('Ctrl Pts',(-1.9401647724022,1.30412254697203,-2.38110351883578));
#55285=CARTESIAN_POINT('Ctrl Pts',(-1.81342265360241,2.7073568271026,-0.201508537622347));
#55286=CARTESIAN_POINT('Ctrl Pts',(-1.68668053480263,1.64225173861224,2.16180494588469));
#55287=CARTESIAN_POINT('Ctrl Pts',(-1.55993841600284,-0.920123533615601,
2.55416617658939));
#55288=CARTESIAN_POINT('Ctrl Pts',(-1.43319629720305,-2.64360199025601,
0.617852663768124));
#55289=CARTESIAN_POINT('Ctrl Pts',(-1.30645417840327,-1.95687614806216,
-1.88176653419882));
#55290=CARTESIAN_POINT('Ctrl Pts',(-1.17971205960348,0.513984726956457,
-2.66574989948821));
#55291=CARTESIAN_POINT('Ctrl Pts',(-1.05296994080369,2.51620021477854,-1.01932414938945));
#55292=CARTESIAN_POINT('Ctrl Pts',(-0.926227822003905,2.22442643942114,
1.55643207734212));
#55293=CARTESIAN_POINT('Ctrl Pts',(-0.799485703204116,-0.0955282270855373,
2.71317130084975));
#55294=CARTESIAN_POINT('Ctrl Pts',(-0.672743584404332,-2.32812986541486,
1.39625479581018));
#55295=CARTESIAN_POINT('Ctrl Pts',(-0.546001465604542,-2.43863094975541,
-1.19362348980373));
#55296=CARTESIAN_POINT('Ctrl Pts',(-0.419259346804758,-0.324852146722302,
-2.6953061211767));
#55297=CARTESIAN_POINT('Ctrl Pts',(-0.292517228004968,2.08330125232009,
-1.73953817690733));
#55298=CARTESIAN_POINT('Ctrl Pts',(-0.165775109205184,2.59553934935526,
0.802002143184149));
#55299=CARTESIAN_POINT('Ctrl Pts',(-0.0390329904053946,0.734480528657613,
2.61278444881232));
#55300=CARTESIAN_POINT('Ctrl Pts',(0.0454617554611288,-0.942240514482439,
2.23100178998994));
#55301=CARTESIAN_POINT('Ctrl Pts',(0.0877091283943909,-1.51564052707394,
1.72809696862439));
#55302=CARTESIAN_POINT('Ctrl Pts',(-9.83720912839439,1.24871913126436,-1.74610375092437));
#55303=CARTESIAN_POINT('Ctrl Pts',(-9.79496175546113,1.82809397593127,-1.33176614221934));
#55304=CARTESIAN_POINT('Ctrl Pts',(-9.71046700959461,2.53222160349819,0.111628485290073));
#55305=CARTESIAN_POINT('Ctrl Pts',(-9.58372489079481,1.2818529339336,2.18943092670103));
#55306=CARTESIAN_POINT('Ctrl Pts',(-9.45698277199503,-1.13827074467732,
2.26472418225056));
#55307=CARTESIAN_POINT('Ctrl Pts',(-9.33024065319525,-2.52005231575915,
0.278422812062161));
#55308=CARTESIAN_POINT('Ctrl Pts',(-9.20349853439546,-1.60455664280285,
-1.96337694338634));
#55309=CARTESIAN_POINT('Ctrl Pts',(-9.07675641559566,0.773993888127739,
-2.41426818657572));
#55310=CARTESIAN_POINT('Ctrl Pts',(-8.9500142967959,2.44680060919036,-0.664486059487474));
#55311=CARTESIAN_POINT('Ctrl Pts',(-8.82327217799609,1.88886231190509,1.69135661119872));
#55312=CARTESIAN_POINT('Ctrl Pts',(-8.69653005919631,-0.391204482481263,
2.50503749356526));
#55313=CARTESIAN_POINT('Ctrl Pts',(-8.56978794039652,-2.31459216016759,
1.034900709349));
#55314=CARTESIAN_POINT('Ctrl Pts',(-8.44304582159674,-2.12773499708311,
-1.37880600196934));
#55315=CARTESIAN_POINT('Ctrl Pts',(-8.31630370279695,-0.00098434116701247,
-2.53541509609748));
#55316=CARTESIAN_POINT('Ctrl Pts',(-8.18956158399716,2.12666207065484,-1.38045481394644));
#55317=CARTESIAN_POINT('Ctrl Pts',(-8.06281946519737,2.31539728853041,1.03309330365651));
#55318=CARTESIAN_POINT('Ctrl Pts',(-7.93607734639759,0.393147027751557,
2.50475102120706));
#55319=CARTESIAN_POINT('Ctrl Pts',(-7.8093352275978,-1.88754147039541,1.69278823095219));
#55320=CARTESIAN_POINT('Ctrl Pts',(-7.68259310879802,-2.44732812325703,
-0.662517576831704));
#55321=CARTESIAN_POINT('Ctrl Pts',(-7.55585098999822,-0.775846225733801,
-2.41379506168045));
#55322=CARTESIAN_POINT('Ctrl Pts',(-7.42910887119844,1.60298714202776,-1.96437689092383));
#55323=CARTESIAN_POINT('Ctrl Pts',(-7.30236675239865,2.52035132183546,0.275995445758637));
#55324=CARTESIAN_POINT('Ctrl Pts',(-7.17562463359886,1.1398705815617,2.26473823369224));
#55325=CARTESIAN_POINT('Ctrl Pts',(-7.04888251479908,-1.27984852959178,
2.18868271047284));
#55326=CARTESIAN_POINT('Ctrl Pts',(-6.92214039599929,-2.53270911678938,
0.117169879155415));
#55327=CARTESIAN_POINT('Ctrl Pts',(-6.7953982771995,-1.47645799134757,-2.06116861120004));
#55328=CARTESIAN_POINT('Ctrl Pts',(-6.66865615839972,0.925903674210762,
-2.36030647122569));
#55329=CARTESIAN_POINT('Ctrl Pts',(-6.54191403959993,2.48410404130888,-0.507514887747857));
#55330=CARTESIAN_POINT('Ctrl Pts',(-6.41517192080014,1.7775067274402,1.8079861953487));
#55331=CARTESIAN_POINT('Ctrl Pts',(-6.28842980200036,-0.549672110652437,
2.47511713269453));
#55332=CARTESIAN_POINT('Ctrl Pts',(-6.16168768320056,-2.37570602866514,
0.885643898355919));
#55333=CARTESIAN_POINT('Ctrl Pts',(-6.03494556440078,-2.0357704806235,-1.51128514831095));
#55334=CARTESIAN_POINT('Ctrl Pts',(-5.908203445601,0.160209816906179,-2.53035117404734));
#55335=CARTESIAN_POINT('Ctrl Pts',(-5.78146132680121,2.21012424291363,-1.24245526287563));
#55336=CARTESIAN_POINT('Ctrl Pts',(-5.65471920800142,2.24503278497613,1.17820713108709));
#55337=CARTESIAN_POINT('Ctrl Pts',(-5.52797708920164,0.233108762821149,
2.52467909922792));
#55338=CARTESIAN_POINT('Ctrl Pts',(-5.40123497040184,-1.99134427447465,
1.56936045250534));
#55339=CARTESIAN_POINT('Ctrl Pts',(-5.27449285160206,-2.40025665025101,
-0.816769405828604));
#55340=CARTESIAN_POINT('Ctrl Pts',(-5.14775073280227,-0.620816362718671,
-2.45823743628542));
#55341=CARTESIAN_POINT('Ctrl Pts',(-5.02100861400248,1.72463220590289,-1.8584907865618));
#55342=CARTESIAN_POINT('Ctrl Pts',(-4.8942664952027,2.49770580344732,0.435671859085126));
#55343=CARTESIAN_POINT('Ctrl Pts',(-4.7675243764029,0.993580774517831,2.33262545083467));
#55344=CARTESIAN_POINT('Ctrl Pts',(-4.64078225760313,-1.41640785608141,
2.10288683352277));
#55345=CARTESIAN_POINT('Ctrl Pts',(-4.51404013880334,-2.53503462174748,
-0.0440875936745136));
#55346=CARTESIAN_POINT('Ctrl Pts',(-4.38729802000355,-1.34242947581622,
-2.15086665133653));
#55347=CARTESIAN_POINT('Ctrl Pts',(-4.26055590120377,1.07409025374736,-2.29666592611456));
#55348=CARTESIAN_POINT('Ctrl Pts',(-4.13381378240397,2.51134459218356,-0.348557869933718));
#55349=CARTESIAN_POINT('Ctrl Pts',(-4.0070716636042,1.65896560068717,1.91733601257026));
#55350=CARTESIAN_POINT('Ctrl Pts',(-3.8803295448044,-0.705919059814479,
2.43516375842623));
#55351=CARTESIAN_POINT('Ctrl Pts',(-3.75358742600462,-2.42720593905067,
0.732813467993737));
#55352=CARTESIAN_POINT('Ctrl Pts',(-3.62684530720482,-1.93557005410118,
-1.63765466901604));
#55353=CARTESIAN_POINT('Ctrl Pts',(-3.50010318840505,0.32075623687857,-2.51504665679077));
#55354=CARTESIAN_POINT('Ctrl Pts',(-3.37336106960525,2.28464389852199,-1.09943008269438));
#55355=CARTESIAN_POINT('Ctrl Pts',(-3.24661895080547,2.16558490516209,1.31855461290034));
#55356=CARTESIAN_POINT('Ctrl Pts',(-3.11987683200568,0.0721272603440025,
2.5343918220449));
#55357=CARTESIAN_POINT('Ctrl Pts',(-2.9931347132059,-2.08708997104618,1.43958317049948));
#55358=CARTESIAN_POINT('Ctrl Pts',(-2.86639259440611,-2.34347364444646,
-0.967716653672553));
#55359=CARTESIAN_POINT('Ctrl Pts',(-2.73965047560632,-0.463274639990797,
-2.4927336116783));
#55360=CARTESIAN_POINT('Ctrl Pts',(-2.61290835680653,1.83929932633204,-1.74508517098032));
#55361=CARTESIAN_POINT('Ctrl Pts',(-2.48616623800675,2.46495444527078,0.593585539410353));
#55362=CARTESIAN_POINT('Ctrl Pts',(-2.35942411920696,0.843270907287779,
2.39107474757259));
#55363=CARTESIAN_POINT('Ctrl Pts',(-2.23268200040717,-1.54723635899034,
2.00858258394327));
#55364=CARTESIAN_POINT('Ctrl Pts',(-2.10593988160738,-2.52710320220323,
-0.205166691235395));
#55365=CARTESIAN_POINT('Ctrl Pts',(-1.9791977628076,-1.20296953518432,-2.23186217762525));
#55366=CARTESIAN_POINT('Ctrl Pts',(-1.85245564400781,1.21793121886668,-2.22373297484717));
#55367=CARTESIAN_POINT('Ctrl Pts',(-1.72571352520802,2.52842373440753,-0.188190549583124));
#55368=CARTESIAN_POINT('Ctrl Pts',(-1.59897140640823,1.53371296764859,2.0189281588656));
#55369=CARTESIAN_POINT('Ctrl Pts',(-1.47222928760845,-0.859311250623144,
2.38535767352872));
#55370=CARTESIAN_POINT('Ctrl Pts',(-1.34548716880866,-2.46888254609704,
0.577017895757046));
#55371=CARTESIAN_POINT('Ctrl Pts',(-1.21874505000888,-1.82754339898057,
-1.75739788713925));
#55372=CARTESIAN_POINT('Ctrl Pts',(-1.09200293120909,0.480014739745447,
-2.48956666826728));
#55373=CARTESIAN_POINT('Ctrl Pts',(-0.965260812409302,2.34990093654407,
-0.951955555533188));
#55374=CARTESIAN_POINT('Ctrl Pts',(-0.838518693609514,2.07741090814953,
1.45356525078249));
#55375=CARTESIAN_POINT('Ctrl Pts',(-0.711776574809726,-0.0892146296531849,
2.53385392125184));
#55376=CARTESIAN_POINT('Ctrl Pts',(-0.585034456009941,-2.17426042609893,
1.3039743153417));
#55377=CARTESIAN_POINT('Ctrl Pts',(-0.458292337210151,-2.27745833541309,
-1.11473520274606));
#55378=CARTESIAN_POINT('Ctrl Pts',(-0.331550218410368,-0.303382202790349,
-2.51716947690649));
#55379=CARTESIAN_POINT('Ctrl Pts',(-0.204808099610577,1.94561288691461,
-1.62456960581273));
#55380=CARTESIAN_POINT('Ctrl Pts',(-0.078065980810793,2.42399643401339,
0.74899667216851));
#55381=CARTESIAN_POINT('Ctrl Pts',(0.0486761379889964,0.685937657913202,
2.44010178013288));
#55382=CARTESIAN_POINT('Ctrl Pts',(0.13317088385552,-0.879966488528001,
2.08355168437591));
#55383=CARTESIAN_POINT('Ctrl Pts',(0.175418256788782,-1.41546967253109,
1.61388456338194));
#55384=CARTESIAN_POINT('Ctrl Pts',(-9.7495,1.16034898466907,-1.62253437445173));
#55385=CARTESIAN_POINT('Ctrl Pts',(-9.70725262706674,1.69872226327124,-1.23751887213913));
#55386=CARTESIAN_POINT('Ctrl Pts',(-9.62275788120021,2.35301974079721,0.103728689921924));
#55387=CARTESIAN_POINT('Ctrl Pts',(-9.49601576240043,1.19113795339939,2.03448789178737));
#55388=CARTESIAN_POINT('Ctrl Pts',(-9.36927364360064,-1.05771687947754,
2.10445274652685));
#55389=CARTESIAN_POINT('Ctrl Pts',(-9.24253152480086,-2.34171165692263,
0.258719210106041));
#55390=CARTESIAN_POINT('Ctrl Pts',(-9.11578940600106,-1.49100436175355,
-1.82443143997822));
#55391=CARTESIAN_POINT('Ctrl Pts',(-8.98904728720129,0.719219398296349,
-2.24341372601176));
#55392=CARTESIAN_POINT('Ctrl Pts',(-8.86230516840148,2.27364387353221,-0.617461289050906));
#55393=CARTESIAN_POINT('Ctrl Pts',(-8.73556304960172,1.75519010714565,1.57166161499472));
#55394=CARTESIAN_POINT('Ctrl Pts',(-8.60882093080191,-0.363519475821205,
2.32775941317825));
#55395=CARTESIAN_POINT('Ctrl Pts',(-8.48207881200213,-2.15079163578927,
0.961662200298393));
#55396=CARTESIAN_POINT('Ctrl Pts',(-8.35533669320235,-1.97715809880351,
-1.28122978529272));
#55397=CARTESIAN_POINT('Ctrl Pts',(-8.22859457440256,-0.000914680687675627,
-2.35598723428903));
#55398=CARTESIAN_POINT('Ctrl Pts',(-8.10185245560277,1.97616110191247,-1.28276191309921));
#55399=CARTESIAN_POINT('Ctrl Pts',(-7.97511033680299,2.15153978631802,0.959982702237039));
#55400=CARTESIAN_POINT('Ctrl Pts',(-7.8483682180032,0.36532454981711,2.32749321407739));
#55401=CARTESIAN_POINT('Ctrl Pts',(-7.7216260992034,-1.75396273978475,1.57299192097447));
#55402=CARTESIAN_POINT('Ctrl Pts',(-7.59488398040363,-2.2741340561492,-0.615632113222856));
#55403=CARTESIAN_POINT('Ctrl Pts',(-7.46814186160383,-0.720940648501152,
-2.24297408351883));
#55404=CARTESIAN_POINT('Ctrl Pts',(-7.34139974280405,1.48954593240367,-1.82536062259485));
#55405=CARTESIAN_POINT('Ctrl Pts',(-7.21465762400426,2.34198950274749,0.256463625198942));
#55406=CARTESIAN_POINT('Ctrl Pts',(-7.08791550520447,1.05920349809169,2.10446580356721));
#55407=CARTESIAN_POINT('Ctrl Pts',(-6.96117338640469,-1.18927539801392,
2.03379262579923));
#55408=CARTESIAN_POINT('Ctrl Pts',(-6.8344312676049,-2.35347275343895,0.108877926915484));
#55409=CARTESIAN_POINT('Ctrl Pts',(-6.70768914880511,-1.37197107682013,
-1.91530252508911));
#55410=CARTESIAN_POINT('Ctrl Pts',(-6.58094703000533,0.860378736396868,
-2.19327080752055));
#55411=CARTESIAN_POINT('Ctrl Pts',(-6.45420491120554,2.30830739273333,-0.471598752640533));
#55412=CARTESIAN_POINT('Ctrl Pts',(-6.32746279240575,1.65171500523044,1.68003748284402));
#55413=CARTESIAN_POINT('Ctrl Pts',(-6.20072067360598,-0.510772566486323,
2.29995647536138));
#55414=CARTESIAN_POINT('Ctrl Pts',(-6.07397855480617,-2.20758055932288,
0.822968089865889));
#55415=CARTESIAN_POINT('Ctrl Pts',(-5.94723643600639,-1.89170178550794,
-1.40433356347513));
#55416=CARTESIAN_POINT('Ctrl Pts',(-5.82049431720661,0.148871987083987,
-2.35128167908273));
#55417=CARTESIAN_POINT('Ctrl Pts',(-5.69375219840681,2.05371677028819,-1.15452840168687));
#55418=CARTESIAN_POINT('Ctrl Pts',(-5.56701007960703,2.08615488253003,1.09482702239254));
#55419=CARTESIAN_POINT('Ctrl Pts',(-5.44026796080724,0.216611974209998,
2.34601100924763));
#55420=CARTESIAN_POINT('Ctrl Pts',(-5.31352584200746,-1.85041956126164,
1.45829895774923));
#55421=CARTESIAN_POINT('Ctrl Pts',(-5.18678372320767,-2.23039376696656,
-0.75896775106054));
#55422=CARTESIAN_POINT('Ctrl Pts',(-5.06004160440788,-0.576882037049555,
-2.28427133200172));
#55423=CARTESIAN_POINT('Ctrl Pts',(-4.93329948560809,1.60258234133143,-1.72696793314944));
#55424=CARTESIAN_POINT('Ctrl Pts',(-4.80655736680831,2.32094657675149,0.404839956945686));
#55425=CARTESIAN_POINT('Ctrl Pts',(-4.67981524800852,0.923266420793207,
2.16754873511761));
#55426=CARTESIAN_POINT('Ctrl Pts',(-4.55307312920873,-1.31617060757069,
1.95406840582431));
#55427=CARTESIAN_POINT('Ctrl Pts',(-4.42633101040895,-2.35563368558887,
-0.0409675749140953));
#55428=CARTESIAN_POINT('Ctrl Pts',(-4.29958889160916,-1.24742757618837,
-1.9986527574939));
#55429=CARTESIAN_POINT('Ctrl Pts',(-4.17284677280937,0.998078354190639,
-2.13413401682469));
#55430=CARTESIAN_POINT('Ctrl Pts',(-4.04610465400959,2.33362016704573,-0.323890905768756));
#55431=CARTESIAN_POINT('Ctrl Pts',(-3.9193625352098,1.54156287203605,1.78164876292292));
#55432=CARTESIAN_POINT('Ctrl Pts',(-3.79262041641001,-0.655962132561314,
2.26283054679536));
#55433=CARTESIAN_POINT('Ctrl Pts',(-3.66587829761022,-2.25543589142298,
0.680953260223828));
#55434=CARTESIAN_POINT('Ctrl Pts',(-3.53913617881044,-1.79859240625076,
-1.52176008587877));
#55435=CARTESIAN_POINT('Ctrl Pts',(-3.41239406001065,0.298056756295131,
-2.33706024159941));
#55436=CARTESIAN_POINT('Ctrl Pts',(-3.28565194121087,2.12296277169725,-1.02162491806891));
#55437=CARTESIAN_POINT('Ctrl Pts',(-3.15890982241107,2.0123294206081,1.22524230469704));
#55438=CARTESIAN_POINT('Ctrl Pts',(-3.03216770361129,0.067022912688436,
2.35503637594289));
#55439=CARTESIAN_POINT('Ctrl Pts',(-2.9054255848115,-1.93938946571943,1.3377058366555));
#55440=CARTESIAN_POINT('Ctrl Pts',(-2.77868346601171,-2.17762921689111,
-0.899232668437894));
#55441=CARTESIAN_POINT('Ctrl Pts',(-2.65194134721193,-0.43048932676473,
-2.31632626019967));
#55442=CARTESIAN_POINT('Ctrl Pts',(-2.52519922841214,1.7091346263358,-1.62158787801847));
#55443=CARTESIAN_POINT('Ctrl Pts',(-2.39845710961236,2.29051298743969,0.551578301896968));
#55444=CARTESIAN_POINT('Ctrl Pts',(-2.27171499081256,0.783593777474662,
2.22186165499399));
#55445=CARTESIAN_POINT('Ctrl Pts',(-2.14497287201278,-1.43774055610062,
1.8664379391246));
#55446=CARTESIAN_POINT('Ctrl Pts',(-2.01823075321299,-2.34826356176781,
-0.190647324848677));
#55447=CARTESIAN_POINT('Ctrl Pts',(-1.89148863441321,-1.11783702498862,
-2.07391634106428));
#55448=CARTESIAN_POINT('Ctrl Pts',(-1.76474651561342,1.13173989076134,-2.06636243085856));
#55449=CARTESIAN_POINT('Ctrl Pts',(-1.63800439681363,2.34949064171247,-0.174872561543903));
#55450=CARTESIAN_POINT('Ctrl Pts',(-1.51126227801384,1.42517419668494,1.87605137184651));
#55451=CARTESIAN_POINT('Ctrl Pts',(-1.38452015921406,-0.798498967630685,
2.21654917046805));
#55452=CARTESIAN_POINT('Ctrl Pts',(-1.25777804041427,-2.29416310193808,
0.536183127745966));
#55453=CARTESIAN_POINT('Ctrl Pts',(-1.13103592161449,-1.69821064989898,
-1.63302924007967));
#55454=CARTESIAN_POINT('Ctrl Pts',(-1.0042938028147,0.446044752534434,-2.31338343704634));
#55455=CARTESIAN_POINT('Ctrl Pts',(-0.87755168401491,2.18360165830961,-0.884586961676926));
#55456=CARTESIAN_POINT('Ctrl Pts',(-0.750809565215123,1.93039537687792,
1.35069842422285));
#55457=CARTESIAN_POINT('Ctrl Pts',(-0.624067446415335,-0.0829010322208286,
2.35453654165394));
#55458=CARTESIAN_POINT('Ctrl Pts',(-0.49732532761555,-2.02039098678301,
1.21169383487321));
#55459=CARTESIAN_POINT('Ctrl Pts',(-0.37058320881576,-2.11628572107077,
-1.03584691568837));
#55460=CARTESIAN_POINT('Ctrl Pts',(-0.243841090015977,-0.281912258858396,
-2.33903283263629));
#55461=CARTESIAN_POINT('Ctrl Pts',(-0.117098971216186,1.80792452150913,
-1.50960103471813));
#55462=CARTESIAN_POINT('Ctrl Pts',(0.00964314758359784,2.25245351867153,
0.695991201152868));
#55463=CARTESIAN_POINT('Ctrl Pts',(0.136385266383387,0.637394787168788,
2.26741911145345));
#55464=CARTESIAN_POINT('Ctrl Pts',(0.220880012249911,-0.817692462573564,
1.93610157876188));
#55465=CARTESIAN_POINT('Ctrl Pts',(0.263127385183173,-1.31529881798823,
1.49967215813949));
#55466=CARTESIAN_POINT('Ctrl Pts',(-3.33066907387547E-16,1.94778769460277,
0.44492227130092));
#55467=CARTESIAN_POINT('Ctrl Pts',(-2.78017970008656E-16,1.94229684361246,
0.495391667149364));
#55468=CARTESIAN_POINT('Ctrl Pts',(-8.36995712052826E-17,1.93476724548118,
0.545536653760479));
#55469=CARTESIAN_POINT('Ctrl Pts',(4.44089209850063E-16,1.92517489938227,
0.595239817297363));
#55470=CARTESIAN_POINT('Ctrl Pts',(1.30360610691075E-15,1.91158592682602,
0.665651676742075));
#55471=CARTESIAN_POINT('Ctrl Pts',(1.86666261596114E-15,1.89385995586343,
0.735177204263595));
#55472=CARTESIAN_POINT('Ctrl Pts',(2.16493489801906E-15,1.87228223168555,
0.803608687878914));
#55473=CARTESIAN_POINT('Ctrl Pts',(2.33682441395151E-15,1.85984733650095,
0.843044650590637));
#55474=CARTESIAN_POINT('Ctrl Pts',(3.09850546232639E-15,1.84613226217488,
0.882117351599893));
#55475=CARTESIAN_POINT('Ctrl Pts',(3.3584246494911E-15,1.83118397114934,
0.92078674243017));
#55476=CARTESIAN_POINT('Ctrl Pts',(3.4512817092519E-15,1.82584364068654,
0.934601520686482));
#55477=CARTESIAN_POINT('Ctrl Pts',(5.14526117317723E-15,1.82034502120261,
0.948366855376327));
#55478=CARTESIAN_POINT('Ctrl Pts',(5.10702591327572E-15,1.81469282599686,
0.962074296960212));
#55479=CARTESIAN_POINT('Ctrl Pts',(4.91398682270459E-15,1.78615647957058,
1.03127932039215));
#55480=CARTESIAN_POINT('Ctrl Pts',(1.57991081056868E-15,1.75376708458297,
1.09887379297229));
#55481=CARTESIAN_POINT('Ctrl Pts',(2.02615701994091E-15,1.71783897253111,
1.16463210299435));
#55482=CARTESIAN_POINT('Ctrl Pts',(2.40198295802782E-15,1.68758052745753,
1.22001336569643));
#55483=CARTESIAN_POINT('Ctrl Pts',(9.6226338214899E-16,1.65481094394572,
1.27409256788157));
#55484=CARTESIAN_POINT('Ctrl Pts',(-1.11022302462516E-16,1.61968946493905,
1.32673151007246));
#55485=CARTESIAN_POINT('Ctrl Pts',(-6.27375591389265E-16,1.60279266713668,
1.35205588671848));
#55486=CARTESIAN_POINT('Ctrl Pts',(1.75865109731242E-15,1.58535115062893,
1.3770468300385));
#55487=CARTESIAN_POINT('Ctrl Pts',(2.08166817117217E-15,1.56738072623534,
1.40168833178254));
#55488=CARTESIAN_POINT('Ctrl Pts',(2.22920138240781E-15,1.55917300400452,
1.41294296869237));
#55489=CARTESIAN_POINT('Ctrl Pts',(2.71625400367046E-15,1.55085356468685,
1.42412649900037));
#55490=CARTESIAN_POINT('Ctrl Pts',(2.74780198594726E-15,1.54242825515624,
1.43523154925794));
#55491=CARTESIAN_POINT('Ctrl Pts',(2.92341485402674E-15,1.49552849598478,
1.49704817222887));
#55492=CARTESIAN_POINT('Ctrl Pts',(-2.81995048998912E-16,1.44546546398451,
1.5562869964589));
#55493=CARTESIAN_POINT('Ctrl Pts',(2.77555756156289E-16,1.39255537912687,
1.61271764417995));
#55494=CARTESIAN_POINT('Ctrl Pts',(8.58082221464105E-16,1.3376618748042,
1.67126368531636));
#55495=CARTESIAN_POINT('Ctrl Pts',(4.15797763651073E-15,1.27970356617436,
1.72678807561908));
#55496=CARTESIAN_POINT('Ctrl Pts',(4.16333634234434E-15,1.21897882333849,
1.77901722439187));
#55497=CARTESIAN_POINT('Ctrl Pts',(4.16735537171954E-15,1.17343526621159,
1.81818908597146));
#55498=CARTESIAN_POINT('Ctrl Pts',(3.33284943214798E-15,1.1263343801715,
1.85550713131994));
#55499=CARTESIAN_POINT('Ctrl Pts',(3.21964677141295E-15,1.07778483301809,
1.89084487676288));
#55500=CARTESIAN_POINT('Ctrl Pts',(3.13474477586169E-15,1.04137267265304,
1.91734818584509));
#55501=CARTESIAN_POINT('Ctrl Pts',(-5.66770666261751E-16,1.00414532731161,
1.94273739803079));
#55502=CARTESIAN_POINT('Ctrl Pts',(-1.2490009027033E-15,0.966144112163664,
1.96695430423757));
#55503=CARTESIAN_POINT('Ctrl Pts',(-1.45112461612772E-15,0.954885527729754,
1.97412902436679));
#55504=CARTESIAN_POINT('Ctrl Pts',(2.39597543965932E-15,0.943558993222492,
1.98120081342834));
#55505=CARTESIAN_POINT('Ctrl Pts',(2.47024622979097E-15,0.93216552638612,
1.9881680745812));
#55506=CARTESIAN_POINT('Ctrl Pts',(2.54570229372929E-15,0.920590233319215,
1.99524652496652));
#55507=CARTESIAN_POINT('Ctrl Pts',(2.81004988937245E-15,0.908953402112989,
2.00221242915967));
#55508=CARTESIAN_POINT('Ctrl Pts',(2.83106871279415E-15,0.897260995259629,
2.00906188950943));
#55509=CARTESIAN_POINT('Ctrl Pts',(2.95672443316249E-15,0.827360897784044,
2.05000965604785));
#55510=CARTESIAN_POINT('Ctrl Pts',(1.01791631789566E-15,0.755427269601269,
2.08682921292429));
#55511=CARTESIAN_POINT('Ctrl Pts',(1.02695629777827E-15,0.681756120222867,
2.11925544414052));
#55512=CARTESIAN_POINT('Ctrl Pts',(1.02998713989497E-15,0.657056328274081,
2.13012701559668));
#55513=CARTESIAN_POINT('Ctrl Pts',(-4.90495785102318E-16,0.632160870785924,
2.14050450196444));
#55514=CARTESIAN_POINT('Ctrl Pts',(-3.05311331771918E-16,0.607079892476986,
2.15037707313459));
#55515=CARTESIAN_POINT('Ctrl Pts',(2.28194171035767E-16,0.534823071221345,
2.17881936918813));
#55516=CARTESIAN_POINT('Ctrl Pts',(-3.84602209731775E-16,0.461028480592185,
2.20307440482459));
#55517=CARTESIAN_POINT('Ctrl Pts',(-7.21644966006352E-16,0.386016998127302,
2.22326012171866));
#55518=CARTESIAN_POINT('Ctrl Pts',(-1.06565834813591E-15,0.309454148753157,
2.24386331407382));
#55519=CARTESIAN_POINT('Ctrl Pts',(2.04973673170663E-17,0.231622791270828,
2.26022731453648));
#55520=CARTESIAN_POINT('Ctrl Pts',(-9.71445146547012E-17,0.152841574836257,
2.27242853705113));
#55521=CARTESIAN_POINT('Ctrl Pts',(-1.25821375813147E-16,0.133637546749305,
2.27540275642055));
#55522=CARTESIAN_POINT('Ctrl Pts',(-1.6506500080672E-16,0.114370082645178,
2.27813013708582));
#55523=CARTESIAN_POINT('Ctrl Pts',(-1.38777878078145E-16,0.0950804498402654,
2.28060703633122));
#55524=CARTESIAN_POINT('Ctrl Pts',(-2.93887515852296E-17,0.0148101173019452,
2.29091420641076));
#55525=CARTESIAN_POINT('Ctrl Pts',(1.50839573175713E-15,-0.0659302194831374,
2.29690448772608));
#55526=CARTESIAN_POINT('Ctrl Pts',(1.72084568816899E-15,-0.146785204436318,
2.2987285654627));
#55527=CARTESIAN_POINT('Ctrl Pts',(1.93752787510066E-15,-0.229250907229958,
2.30058898078018));
#55528=CARTESIAN_POINT('Ctrl Pts',(1.87752606053914E-15,-0.31183670491661,
2.29811569375814));
#55529=CARTESIAN_POINT('Ctrl Pts',(2.78943534937071E-15,-0.394188581132097,
2.29141818620213));
#55530=CARTESIAN_POINT('Ctrl Pts',(3.70842065500646E-15,-0.477179471849459,
2.28466870891997));
#55531=CARTESIAN_POINT('Ctrl Pts',(1.18560937916683E-15,-0.559933765294961,
2.27362925411048));
#55532=CARTESIAN_POINT('Ctrl Pts',(1.08246744900953E-15,-0.642098510266275,
2.25835984156219));
#55533=CARTESIAN_POINT('Ctrl Pts',(1.03867200960394E-15,-0.676986757016934,
2.251876245308));
#55534=CARTESIAN_POINT('Ctrl Pts',(2.77700457960347E-15,-0.711768739488473,
2.2446293603931));
#55535=CARTESIAN_POINT('Ctrl Pts',(2.94902990916057E-15,-0.746417272235456,
2.2366209401127));
#55536=CARTESIAN_POINT('Ctrl Pts',(3.03536878136454E-15,-0.763807241774236,
2.23260154380097));
#55537=CARTESIAN_POINT('Ctrl Pts',(9.62922053153124E-16,-0.781168224136483,
2.22838899571903));
#55538=CARTESIAN_POINT('Ctrl Pts',(9.64506252643105E-16,-0.798467774965364,
2.22399107243053));
#55539=CARTESIAN_POINT('Ctrl Pts',(9.72126262098133E-16,-0.881678722650616,
2.20283703390646));
#55540=CARTESIAN_POINT('Ctrl Pts',(-3.22349389677964E-15,-0.963583670002293,
2.17737390106192));
#55541=CARTESIAN_POINT('Ctrl Pts',(-2.8796409701215E-15,-1.04381049082807,
2.14772461235836));
#55542=CARTESIAN_POINT('Ctrl Pts',(-2.53522490946127E-15,-1.12416870053318,
2.1180267664918));
#55543=CARTESIAN_POINT('Ctrl Pts',(1.71723154797487E-15,-1.20284431254245,
2.08412900274903));
#55544=CARTESIAN_POINT('Ctrl Pts',(2.46330733588707E-15,-1.27946633222789,
2.0461027486611));
#55545=CARTESIAN_POINT('Ctrl Pts',(3.19367717044613E-15,-1.3544753497405,
2.00887700114715));
#55546=CARTESIAN_POINT('Ctrl Pts',(-9.56957227323442E-16,-1.42751726659118,
1.9676945422236));
#55547=CARTESIAN_POINT('Ctrl Pts',(-1.46410661372443E-15,-1.4982323415318,
1.92257464684908));
#55548=CARTESIAN_POINT('Ctrl Pts',(-1.75068212599161E-15,-1.53819139377464,
1.89707869343356));
#55549=CARTESIAN_POINT('Ctrl Pts',(-1.59168655826546E-16,-1.57740718395233,
1.87032464339947));
#55550=CARTESIAN_POINT('Ctrl Pts',(-2.77555756156289E-17,-1.6158113816168,
1.84230937386684));
#55551=CARTESIAN_POINT('Origin',(2.95,-2.77555756156289E-16,-1.73205080756888));
#55552=CARTESIAN_POINT('',(2.6551551490412,-3.18172571617472E-16,-1.73205080756888));
#55553=CARTESIAN_POINT('',(2.6551551490412,-1.5,-0.866025403784439));
#55554=CARTESIAN_POINT('Ctrl Pts',(2.6551551490412,-3.12250225675825E-16,
-1.73205080756888));
#55555=CARTESIAN_POINT('Ctrl Pts',(2.69311148359047,-0.255925908896418,
-1.58429191517493));
#55556=CARTESIAN_POINT('Ctrl Pts',(2.70817242652387,-0.510403274945606,
-1.43736933938377));
#55557=CARTESIAN_POINT('Ctrl Pts',(2.70817242652387,-0.989596725054395,
-1.16070687196955));
#55558=CARTESIAN_POINT('Ctrl Pts',(2.69311148359047,-1.24407409110358,-1.01378429617839));
#55559=CARTESIAN_POINT('Ctrl Pts',(2.6551551490412,-1.5,-0.866025403784439));
#55560=CARTESIAN_POINT('',(0.75,-2.77555756156289E-16,-1.73205080756888));
#55561=CARTESIAN_POINT('',(2.95,-3.18172571617472E-16,-1.73205080756888));
#55562=CARTESIAN_POINT('',(0.75,-1.5,-0.866025403784439));
#55563=CARTESIAN_POINT('',(0.75,-1.5,-0.866025403784439));
#55564=CARTESIAN_POINT('',(2.95,-1.5,-0.866025403784439));
#55565=CARTESIAN_POINT('Origin',(2.95,-1.5,-0.866025403784439));
#55566=CARTESIAN_POINT('',(2.6551551490412,-1.5,0.866025403784439));
#55567=CARTESIAN_POINT('Ctrl Pts',(2.6551551490412,-1.5,-0.866025403784439));
#55568=CARTESIAN_POINT('Ctrl Pts',(2.69311148359047,-1.5,-0.570507618996547));
#55569=CARTESIAN_POINT('Ctrl Pts',(2.70817242652387,-1.5,-0.276662467414215));
#55570=CARTESIAN_POINT('Ctrl Pts',(2.70817242652387,-1.5,0.276662467414215));
#55571=CARTESIAN_POINT('Ctrl Pts',(2.69311148359047,-1.5,0.570507618996546));
#55572=CARTESIAN_POINT('Ctrl Pts',(2.6551551490412,-1.5,0.866025403784439));
#55573=CARTESIAN_POINT('',(0.75,-1.5,0.866025403784439));
#55574=CARTESIAN_POINT('',(0.75,-1.5,0.866025403784439));
#55575=CARTESIAN_POINT('',(2.95,-1.5,0.866025403784439));
#55576=CARTESIAN_POINT('Origin',(2.95,-1.5,0.866025403784439));
#55577=CARTESIAN_POINT('',(2.6551551490412,1.06057523872491E-16,1.73205080756888));
#55578=CARTESIAN_POINT('Ctrl Pts',(2.6551551490412,-1.5,0.866025403784439));
#55579=CARTESIAN_POINT('Ctrl Pts',(2.69311148359047,-1.24407409110358,1.01378429617838));
#55580=CARTESIAN_POINT('Ctrl Pts',(2.70817242652387,-0.989596725054395,
1.16070687196955));
#55581=CARTESIAN_POINT('Ctrl Pts',(2.70817242652387,-0.510403274945606,
1.43736933938377));
#55582=CARTESIAN_POINT('Ctrl Pts',(2.69311148359047,-0.255925908896417,
1.58429191517493));
#55583=CARTESIAN_POINT('Ctrl Pts',(2.6551551490412,3.46944695195361E-17,
1.73205080756888));
#55584=CARTESIAN_POINT('',(0.75,0.,1.73205080756888));
#55585=CARTESIAN_POINT('',(0.75,1.06057523872491E-16,1.73205080756888));
#55586=CARTESIAN_POINT('',(2.95,1.06057523872491E-16,1.73205080756888));
#55587=CARTESIAN_POINT('Origin',(2.95,0.,1.73205080756888));
#55588=CARTESIAN_POINT('',(2.6551551490412,1.5,0.866025403784439));
#55589=CARTESIAN_POINT('Ctrl Pts',(2.6551551490412,1.04083408558608E-16,
1.73205080756888));
#55590=CARTESIAN_POINT('Ctrl Pts',(2.69311148359047,0.255925908896417,1.58429191517493));
#55591=CARTESIAN_POINT('Ctrl Pts',(2.70817242652387,0.510403274945606,1.43736933938377));
#55592=CARTESIAN_POINT('Ctrl Pts',(2.70817242652387,0.989596725054395,1.16070687196955));
#55593=CARTESIAN_POINT('Ctrl Pts',(2.69311148359047,1.24407409110358,1.01378429617838));
#55594=CARTESIAN_POINT('Ctrl Pts',(2.6551551490412,1.5,0.866025403784438));
#55595=CARTESIAN_POINT('',(0.75,1.5,0.866025403784439));
#55596=CARTESIAN_POINT('',(0.75,1.5,0.866025403784439));
#55597=CARTESIAN_POINT('',(2.95,1.5,0.866025403784439));
#55598=CARTESIAN_POINT('Origin',(2.95,1.5,-0.866025403784439));
#55599=CARTESIAN_POINT('',(2.6551551490412,1.5,-0.866025403784439));
#55600=CARTESIAN_POINT('Ctrl Pts',(2.6551551490412,1.5,-0.866025403784439));
#55601=CARTESIAN_POINT('Ctrl Pts',(2.69311148359047,1.24407409110358,-1.01378429617839));
#55602=CARTESIAN_POINT('Ctrl Pts',(2.70817242652387,0.989596725054393,-1.16070687196955));
#55603=CARTESIAN_POINT('Ctrl Pts',(2.70817242652387,0.510403274945605,-1.43736933938377));
#55604=CARTESIAN_POINT('Ctrl Pts',(2.69311148359047,0.255925908896417,-1.58429191517493));
#55605=CARTESIAN_POINT('Ctrl Pts',(2.6551551490412,-2.08166817117217E-16,
-1.73205080756888));
#55606=CARTESIAN_POINT('',(0.75,1.5,-0.866025403784439));
#55607=CARTESIAN_POINT('',(2.95,1.5,-0.866025403784439));
#55608=CARTESIAN_POINT('',(0.75,-3.18172571617472E-16,-1.73205080756888));
#55609=CARTESIAN_POINT('Origin',(2.95,1.5,0.866025403784439));
#55610=CARTESIAN_POINT('Ctrl Pts',(2.6551551490412,1.5,0.866025403784439));
#55611=CARTESIAN_POINT('Ctrl Pts',(2.69311148359047,1.5,0.570507618996546));
#55612=CARTESIAN_POINT('Ctrl Pts',(2.70817242652387,1.5,0.276662467414214));
#55613=CARTESIAN_POINT('Ctrl Pts',(2.70817242652387,1.5,-0.276662467414215));
#55614=CARTESIAN_POINT('Ctrl Pts',(2.69311148359047,1.5,-0.570507618996547));
#55615=CARTESIAN_POINT('Ctrl Pts',(2.6551551490412,1.5,-0.866025403784439));
#55616=CARTESIAN_POINT('',(0.75,1.5,-0.866025403784439));
#55617=CARTESIAN_POINT('Origin',(0.75,0.,0.));
#55618=CARTESIAN_POINT('Origin',(-10.,2.2,0.));
#55619=CARTESIAN_POINT('',(-10.,-2.2,-2.69422295812418E-16));
#55620=CARTESIAN_POINT('Origin',(-10.,0.,0.));
#55621=CARTESIAN_POINT('Origin',(-9.85,0.,0.));
#55622=CARTESIAN_POINT('',(-9.85,-2.35,-2.87791997799628E-16));
#55623=CARTESIAN_POINT('Origin',(-4.85,0.,0.));
#55624=CARTESIAN_POINT('Origin',(0.,0.,0.));
#55625=CARTESIAN_POINT('Origin',(0.,4.75,0.));
#55626=CARTESIAN_POINT('',(0.,-5.81707229594993E-16,4.75));
#55627=CARTESIAN_POINT('Origin',(0.,0.,0.));
#55628=CARTESIAN_POINT('Ctrl Pts',(0.,0.,4.75));
#55629=CARTESIAN_POINT('Ctrl Pts',(0.,-4.75,4.75));
#55630=CARTESIAN_POINT('Ctrl Pts',(0.,-4.75,0.));
#55631=CARTESIAN_POINT('Ctrl Pts',(0.,-4.75,-4.75));
#55632=CARTESIAN_POINT('Ctrl Pts',(0.,0.,-4.75));
#55633=CARTESIAN_POINT('Ctrl Pts',(0.,4.75,-4.75));
#55634=CARTESIAN_POINT('Ctrl Pts',(0.,4.75,0.));
#55635=CARTESIAN_POINT('Ctrl Pts',(0.,4.75,4.75));
#55636=CARTESIAN_POINT('Ctrl Pts',(0.,0.,4.75));
#55637=CARTESIAN_POINT('Ctrl Pts',(2.23533561342085,0.,3.85933086966187));
#55638=CARTESIAN_POINT('Ctrl Pts',(2.23533561342085,-3.85933086966187,3.85933086966187));
#55639=CARTESIAN_POINT('Ctrl Pts',(2.23533561342085,-3.85933086966187,0.));
#55640=CARTESIAN_POINT('Ctrl Pts',(2.23533561342085,-3.85933086966187,-3.85933086966187));
#55641=CARTESIAN_POINT('Ctrl Pts',(2.23533561342085,0.,-3.85933086966187));
#55642=CARTESIAN_POINT('Ctrl Pts',(2.23533561342085,3.85933086966187,-3.85933086966187));
#55643=CARTESIAN_POINT('Ctrl Pts',(2.23533561342085,3.85933086966187,0.));
#55644=CARTESIAN_POINT('Ctrl Pts',(2.23533561342085,3.85933086966187,3.85933086966187));
#55645=CARTESIAN_POINT('Ctrl Pts',(2.23533561342085,0.,3.85933086966187));
#55646=CARTESIAN_POINT('Ctrl Pts',(2.70817242652387,0.,1.5));
#55647=CARTESIAN_POINT('Ctrl Pts',(2.70817242652387,-1.5,1.5));
#55648=CARTESIAN_POINT('Ctrl Pts',(2.70817242652387,-1.5,0.));
#55649=CARTESIAN_POINT('Ctrl Pts',(2.70817242652387,-1.5,-1.5));
#55650=CARTESIAN_POINT('Ctrl Pts',(2.70817242652387,0.,-1.5));
#55651=CARTESIAN_POINT('Ctrl Pts',(2.70817242652387,1.5,-1.5));
#55652=CARTESIAN_POINT('Ctrl Pts',(2.70817242652387,1.5,0.));
#55653=CARTESIAN_POINT('Ctrl Pts',(2.70817242652387,1.5,1.5));
#55654=CARTESIAN_POINT('Ctrl Pts',(2.70817242652387,0.,1.5));
#55655=CARTESIAN_POINT('Ctrl Pts',(2.6551551490412,0.,1.73205080756888));
#55656=CARTESIAN_POINT('Ctrl Pts',(2.09425930345968,0.,3.91554270360305));
#55657=CARTESIAN_POINT('Ctrl Pts',(0.,0.,4.75));
#55714=UNCERTAINTY_MEASURE_WITH_UNIT(LENGTH_MEASURE(0.01),#55738,
'DISTANCE_ACCURACY_VALUE',
'Maximum model space distance between geometric entities at asserted c
onnectivities');
#55715=UNCERTAINTY_MEASURE_WITH_UNIT(LENGTH_MEASURE(0.01),#55738,
'DISTANCE_ACCURACY_VALUE',
'Maximum model space distance between geometric entities at asserted c
onnectivities');
#55736=(
GEOMETRIC_REPRESENTATION_CONTEXT(3)
GLOBAL_UNCERTAINTY_ASSIGNED_CONTEXT((#55714))
GLOBAL_UNIT_ASSIGNED_CONTEXT((#55738,#55740,#55741))
REPRESENTATION_CONTEXT('','3D')
);
#55737=(
GEOMETRIC_REPRESENTATION_CONTEXT(3)
GLOBAL_UNCERTAINTY_ASSIGNED_CONTEXT((#55715))
GLOBAL_UNIT_ASSIGNED_CONTEXT((#55738,#55740,#55741))
REPRESENTATION_CONTEXT('','3D')
);
#55738=(
LENGTH_UNIT()
NAMED_UNIT(*)
SI_UNIT(.MILLI.,.METRE.)
);
#55740=(
NAMED_UNIT(*)
PLANE_ANGLE_UNIT()
SI_UNIT($,.RADIAN.)
);
#55741=(
NAMED_UNIT(*)
SI_UNIT($,.STERADIAN.)
SOLID_ANGLE_UNIT()
);
#55762=SHAPE_DEFINITION_REPRESENTATION(#55783,#55840);
#55783=PRODUCT_DEFINITION_SHAPE('',$,#55862);
#55840=SHAPE_REPRESENTATION('',(#29892),#55736);
#55841=PRODUCT_DEFINITION_CONTEXT('part definition',#55906,'design');
#55862=PRODUCT_DEFINITION('2026-10-26-00-34-39-424',
'19_Window_Screw_ISO_7380_M5x10',#55883,#55841);
#55883=PRODUCT_DEFINITION_FORMATION('',$,#55928);
#55906=APPLICATION_CONTEXT(
'Core Data for Automotive Mechanical Design Process');
#55907=PRODUCT_CONTEXT('part definition',#55906,'mechanical');
#55928=PRODUCT('2026-10-26-00-34-39-424',
'19_Window_Screw_ISO_7380_M5x10',$,(#55907));
#55992=COLOUR_RGB('Black',0.12,0.14,0.17);
#55993=FILL_AREA_STYLE_COLOUR('',#55992);
#55994=FILL_AREA_STYLE('',(#55993));
#55995=SURFACE_STYLE_FILL_AREA(#55994);
#55996=SURFACE_SIDE_STYLE('',(#55995));
#55997=SURFACE_STYLE_USAGE(.BOTH.,#55996);
#55998=PRESENTATION_STYLE_ASSIGNMENT((#55997));
ENDSEC;
END-ISO-10303-21;
